ISO-10303-21;
HEADER;
FILE_DESCRIPTION (('STEP AP214'),
    '1' );
FILE_NAME ('Stem Lock Nut.step',
    '2026-10-09T13:48:35',
    ( '' ),
    ( '' ),
    'SwSTEP 2.0',
    'SolidWorks 2026',
    '' );
FILE_SCHEMA (( 'AUTOMOTIVE_DESIGN' ));
ENDSEC;

DATA;
#15=DIRECTION ( 'NONE',  ( 0.000000000000000000, 0.000000000000000000, 1.000000000000000000 ) ) ;
#31=CARTESIAN_POINT ( 'NONE',  ( 0.000000000000000000, 28.00000000000000000, 0.000000000000000000 ) ) ;
#67=CARTESIAN_POINT ( 'NONE',  ( 0.000000000000000000, 29.85000000000000142, 0.000000000000000000 ) ) ;
#83=ORIENTED_EDGE ( 'NONE', *, *, #21982, .F. ) ;
#134=CARTESIAN_POINT ( 'NONE',  ( -2.000000000000000000, 30.00000000000000000, -3.464101615137999968 ) ) ;
#142=CARTESIAN_POINT ( 'NONE',  ( 0.1752525089982897022, 28.25094615491967787, -4.517620070270786492 ) ) ;
#193=DIRECTION ( 'NONE',  ( 0.000000000000000000, 0.000000000000000000, -1.000000000000000000 ) ) ;
#201=DIRECTION ( 'NONE',  ( 1.000000000000000000, 0.000000000000000000, 0.000000000000000000 ) ) ;
#216=ORIENTED_EDGE ( 'NONE', *, *, #13652, .F. ) ;
#255=ORIENTED_EDGE ( 'NONE', *, *, #14267, .T. ) ;
#260=CARTESIAN_POINT ( 'NONE',  ( 2.000000000000000000, 28.00000000000000000, -3.464101615137999968 ) ) ;
#321=DIRECTION ( 'NONE',  ( -0.5000000000000169864, 0.000000000000000000, 0.8660254037844289376 ) ) ;
#327=ORIENTED_EDGE ( 'NONE', *, *, #12498, .T. ) ;
#333=EDGE_CURVE ( 'NONE', #8084, #19340, #13286, .T. ) ;
#384=DIRECTION ( 'NONE',  ( 0.000000000000000000, 1.000000000000000000, 0.000000000000000000 ) ) ;
#421=ORIENTED_EDGE ( 'NONE', *, *, #1138, .T. ) ;
#444=CARTESIAN_POINT ( 'NONE',  ( 3.025523437588010012, 29.91693820796410463, 2.872015382385962656 ) ) ;
#456=DIRECTION ( 'NONE',  ( -0.000000000000000000, 1.000000000000000000, 0.000000000000000000 ) ) ;
#516=ORIENTED_EDGE ( 'NONE', *, *, #16185, .F. ) ;
#547=CARTESIAN_POINT ( 'NONE',  ( -4.000000000000000000, 29.92936170367562809, -1.090349405812125694 ) ) ;
#552=CARTESIAN_POINT ( 'NONE',  ( 4.000000000000000000, 29.81534065533123723, -1.802053058880664471 ) ) ;
#584=DIRECTION ( 'NONE',  ( 0.000000000000000000, 1.000000000000000000, 0.000000000000000000 ) ) ;
#593=CARTESIAN_POINT ( 'NONE',  ( 2.399999999999999911, 30.00000000000000000, 0.000000000000000000 ) ) ;
#594=B_SPLINE_CURVE_WITH_KNOTS ( 'NONE', 3,
 ( #15681, #11956, #10132, #23200, #19208, #22833, #547, #673, #21282, #4692 ),
 .UNSPECIFIED., .F., .F.,
 ( 4, 1, 1, 2, 2, 4 ),
 ( 0.000000000000000000, 0.2500000000000001110, 0.3750000000000002776, 0.4375000000000004441, 0.5000000000000005551, 1.000000000000000000 ),
 .UNSPECIFIED. ) ;
#598=ORIENTED_EDGE ( 'NONE', *, *, #22681, .F. ) ;
#658=LINE ( 'NONE', #11344, #22673 ) ;
#668=EDGE_CURVE ( 'NONE', #9155, #14280, #5034, .T. ) ;
#673=CARTESIAN_POINT ( 'NONE',  ( -4.000000000000000000, 29.87418302490046784, -1.506880184559495239 ) ) ;
#689=PRODUCT_DEFINITION_SHAPE ( 'NONE', 'NONE',  #1482 ) ;
#708=AXIS2_PLACEMENT_3D ( 'NONE', #10789, #16573, #20224 ) ;
#715=AXIS2_PLACEMENT_3D ( 'NONE', #6015, #15457, #201 ) ;
#771=ORIENTED_EDGE ( 'NONE', *, *, #23253, .T. ) ;
#781=FACE_OUTER_BOUND ( 'NONE', #7651, .T. ) ;
#802=CARTESIAN_POINT ( 'NONE',  ( 4.000000000000000000, 29.91693820796410108, -1.184172465503444904 ) ) ;
#815=DIRECTION ( 'NONE',  ( 0.000000000000000000, 1.000000000000000000, 0.000000000000000000 ) ) ;
#834=CARTESIAN_POINT ( 'NONE',  ( -4.000000000000000888, 30.00000000000001066, 0.3708744353061897425 ) ) ;
#848=ORIENTED_EDGE ( 'NONE', *, *, #23627, .T. ) ;
#921=AXIS2_PLACEMENT_3D ( 'NONE', #17629, #21135, #23186 ) ;
#946=EDGE_CURVE ( 'NONE', #4163, #21630, #17247, .T. ) ;
#954=EDGE_CURVE ( 'NONE', #9155, #6884, #15198, .T. ) ;
#989=CARTESIAN_POINT ( 'NONE',  ( 3.649794085728314208, 28.20197603011189713, -2.511592555635394852 ) ) ;
#990=CARTESIAN_POINT ( 'NONE',  ( -1.672509921847626257, 28.00639765414753413, -3.652834497694421589 ) ) ;
#1023=AXIS2_PLACEMENT_3D ( 'NONE', #10492, #4549, #1278 ) ;
#1046=CARTESIAN_POINT ( 'NONE',  ( 3.999999999999999112, 29.91068681084913905, -1.228746328088897721 ) ) ;
#1097=DIRECTION ( 'NONE',  ( 0.000000000000000000, 0.000000000000000000, -1.000000000000000000 ) ) ;
#1111=VECTOR ( 'NONE', #3507, 1000.000000000000114 ) ;
#1112=CARTESIAN_POINT ( 'NONE',  ( 0.000000000000000000, 29.69999999999999929, 0.000000000000000000 ) ) ;
#1123=DIRECTION ( 'NONE',  ( 8.117316429522999705E-13, 1.000000000000000000, 5.625558360782999934E-11 ) ) ;
#1138=EDGE_CURVE ( 'NONE', #20052, #18819, #14065, .T. ) ;
#1141=VECTOR ( 'NONE', #11951, 1000.000000000000000 ) ;
#1159=DIRECTION ( 'NONE',  ( 0.000000000000000000, 1.000000000000000000, 0.000000000000000000 ) ) ;
#1164=DIRECTION ( 'NONE',  ( 0.000000000000000000, -1.000000000000000000, 0.000000000000000000 ) ) ;
#1212=FACE_OUTER_BOUND ( 'NONE', #2416, .T. ) ;
#1256=CARTESIAN_POINT ( 'NONE',  ( 0.3502059142680099546, 28.20197603011301624, 4.416610674642952539 ) ) ;
#1278=DIRECTION ( 'NONE',  ( 1.000000000000000000, 0.000000000000000000, 0.000000000000000000 ) ) ;
#1288=AXIS2_PLACEMENT_3D ( 'NONE', #15227, #5683, #9443 ) ;
#1320=CARTESIAN_POINT ( 'NONE',  ( 2.649379677055639259, 28.02555747447238943, 3.089210087447479491 ) ) ;
#1364=AXIS2_PLACEMENT_3D ( 'NONE', #11045, #22067, #15 ) ;
#1372=ORIENTED_EDGE ( 'NONE', *, *, #11941, .F. ) ;
#1382=ORIENTED_EDGE ( 'NONE', *, *, #7490, .F. ) ;
#1476=DIRECTION ( 'NONE',  ( 0.000000000000000000, 0.000000000000000000, -1.000000000000000000 ) ) ;
#1482=PRODUCT_DEFINITION ( 'UNKNOWN', '', #2071, #16754 ) ;
#1494=CONICAL_SURFACE ( 'NONE', #19680, 4.309401076758999416, 1.119376321708719590 ) ;
#1511=CARTESIAN_POINT ( 'NONE',  ( 1.670409819843222898, 27.99999999999985079, -3.654390594373847723 ) ) ;
#1530=ORIENTED_EDGE ( 'NONE', *, *, #10282, .F. ) ;
#1613=CARTESIAN_POINT ( 'NONE',  ( 2.100000000000000089, 28.30000000000000071, 0.000000000000000000 ) ) ;
#1670=DIRECTION ( 'NONE',  ( 0.000000000000000000, 1.000000000000000000, 0.000000000000000000 ) ) ;
#1714=AXIS2_PLACEMENT_3D ( 'NONE', #10682, #18068, #1476 ) ;
#1732=CIRCLE ( 'NONE', #9456, 4.000000000000000000 ) ;
#1777=CARTESIAN_POINT ( 'NONE',  ( -0.9358744650684699407, 29.91068681084918879, 4.078474779182606369 ) ) ;
#1790=ORIENTED_EDGE ( 'NONE', *, *, #9816, .F. ) ;
#1854=DIRECTION ( 'NONE',  ( 0.000000000000000000, -0.7071067811866525998, -0.7071067811864425456 ) ) ;
#1931=DIRECTION ( 'NONE',  ( 0.000000000000000000, 0.000000000000000000, 1.000000000000000000 ) ) ;
#1961=CARTESIAN_POINT ( 'NONE',  ( 0.7318187998270078154, 29.87490599056237528, -4.196286372439439027 ) ) ;
#2023=ORIENTED_EDGE ( 'NONE', *, *, #15286, .T. ) ;
#2026=CARTESIAN_POINT ( 'NONE',  ( -3.999878274658705823, 28.13336607547242352, 1.519686587934141242 ) ) ;
#2028=EDGE_CURVE ( 'NONE', #3203, #18824, #5426, .T. ) ;
#2059=CARTESIAN_POINT ( 'NONE',  ( 4.000000000000000000, 29.79977277844472994, 1.897803675662218970 ) ) ;
#2071=PRODUCT_DEFINITION_FORMATION_WITH_SPECIFIED_SOURCE ( 'ANY', '', #17128, .NOT_KNOWN. ) ;
#2077=DIRECTION ( 'NONE',  ( 0.000000000000000000, 1.000000000000000000, 0.000000000000000000 ) ) ;
#2080=CARTESIAN_POINT ( 'NONE',  ( -2.000000000000000000, 28.00000000000000000, -3.464101615137999968 ) ) ;
#2084=ORIENTED_EDGE ( 'NONE', *, *, #954, .T. ) ;
#2139=CARTESIAN_POINT ( 'NONE',  ( -2.404489386789160132, 29.99040384242091406, 3.230569558791225315 ) ) ;
#2192=CARTESIAN_POINT ( 'NONE',  ( -4.000000000000000000, 28.30000000000000071, -2.309401076759000304 ) ) ;
#2257=CONICAL_SURFACE ( 'NONE', #7289, 4.309401076758999416, 1.119376321708719590 ) ;
#2268=DIRECTION ( 'NONE',  ( 0.000000000000000000, 1.000000000000000000, 0.000000000000000000 ) ) ;
#2295=FACE_OUTER_BOUND ( 'NONE', #18594, .T. ) ;
#2369=CARTESIAN_POINT ( 'NONE',  ( 2.000000000000000000, 30.00000000000000000, 3.464101615137999968 ) ) ;
#2408=CIRCLE ( 'NONE', #15543, 4.000000000000000000 ) ;
#2416=EDGE_LOOP ( 'NONE', ( #22277, #16261, #11059 ) ) ;
#2418=CARTESIAN_POINT ( 'NONE',  ( 2.399999988616999591, 28.00000001138332806, 6.337991288364001799E-08 ) ) ;
#2428=VECTOR ( 'NONE', #22513, 1000.000000000000000 ) ;
#2429=CARTESIAN_POINT ( 'NONE',  ( -3.649794085728321758, 28.20197603011191134, 2.511592555635382418 ) ) ;
#2430=VERTEX_POINT ( 'NONE', #12061 ) ;
#2442=CARTESIAN_POINT ( 'NONE',  ( 2.404489386789160132, 29.99040384242091406, -3.230569558791225315 ) ) ;
#2498=ADVANCED_FACE ( 'NONE', ( #781 ), #8670, .T. ) ;
#2553=CARTESIAN_POINT ( 'NONE',  ( -3.653528746112522541, 28.20780860099737097, -2.509315635920815524 ) ) ;
#2561=CARTESIAN_POINT ( 'NONE',  ( 2.817565069457256932, 29.94682129341587284, -2.992080202207098694 ) ) ;
#2571=CARTESIAN_POINT ( 'NONE',  ( -2.000000000000000000, 28.00000000000000000, -3.464101615137999968 ) ) ;
#2639=CARTESIAN_POINT ( 'NONE',  ( 3.064125534931650296, 29.91068681084919234, 2.849728451093327397 ) ) ;
#2645=AXIS2_PLACEMENT_3D ( 'NONE', #13023, #3706, #11227 ) ;
#2666=AXIS2_PLACEMENT_3D ( 'NONE', #9687, #584, #17068 ) ;
#2699=DIRECTION ( 'NONE',  ( 0.000000000000000000, -1.000000000000000000, 0.000000000000000000 ) ) ;
#2712=AXIS2_PLACEMENT_3D ( 'NONE', #14859, #2268, #321 ) ;
#2717=FACE_OUTER_BOUND ( 'NONE', #17296, .T. ) ;
#2764=DIRECTION ( 'NONE',  ( 0.000000000000000000, -1.000000000000000000, 0.000000000000000000 ) ) ;
#2795=FILL_AREA_STYLE ('',( #22995 ) ) ;
#2818=CARTESIAN_POINT ( 'NONE',  ( 3.304996520289661177, 29.87418302490023692, -2.710661522857509276 ) ) ;
#2861=CARTESIAN_POINT ( 'NONE',  ( 3.999878274658704047, 28.13336607547242352, -1.519686587934146349 ) ) ;
#2918=ADVANCED_FACE ( 'NONE', ( #14315 ), #9062, .T. ) ;
#3014=CARTESIAN_POINT ( 'NONE',  ( 0.000000000000000000, 30.00000000000000000, -2.399999999999951950 ) ) ;
#3106=B_SPLINE_CURVE_WITH_KNOTS ( 'NONE', 3,
 ( #16326, #9422, #19977, #16793, #12821, #3397, #16562, #12927 ),
 .UNSPECIFIED., .F., .F.,
 ( 4, 2, 2, 4 ),
 ( 0.000000000000000000, 0.2500000000000000000, 0.5000000000000000000, 1.000000000000000000 ),
 .UNSPECIFIED. ) ;
#3162=ORIENTED_EDGE ( 'NONE', *, *, #14438, .F. ) ;
#3165=FACE_OUTER_BOUND ( 'NONE', #16934, .T. ) ;
#3172=ORIENTED_EDGE ( 'NONE', *, *, #12517, .F. ) ;
#3184=CARTESIAN_POINT ( 'NONE',  ( -4.000000000000000000, 29.69999999999999929, -2.309401076759000304 ) ) ;
#3186=DIRECTION ( 'NONE',  ( 0.5000000000000169864, 0.000000000000000000, 0.8660254037844289376 ) ) ;
#3203=VERTEX_POINT ( 'NONE', #4233 ) ;
#3210=VERTEX_POINT ( 'NONE', #18995 ) ;
#3231=CARTESIAN_POINT ( 'NONE',  ( 4.000000000000000000, 28.00000000000000000, 0.000000000000000000 ) ) ;
#3232=CARTESIAN_POINT ( 'NONE',  ( 0.000000000000000000, 29.69999999999999929, -4.618802153517000519 ) ) ;
#3252=ORIENTED_EDGE ( 'NONE', *, *, #12194, .F. ) ;
#3284=DIRECTION ( 'NONE',  ( 1.000000000000000000, 0.000000000000000000, 0.000000000000000000 ) ) ;
#3295=CARTESIAN_POINT ( 'NONE',  ( 2.399999999999999911, 28.00000000000000000, 0.000000000000000000 ) ) ;
#3297=FACE_OUTER_BOUND ( 'NONE', #3849, .T. ) ;
#3333=CARTESIAN_POINT ( 'NONE',  ( 0.000000000000000000, 30.00000000000000000, 0.000000000000000000 ) ) ;
#3352=ORIENTED_EDGE ( 'NONE', *, *, #5980, .F. ) ;
#3397=CARTESIAN_POINT ( 'NONE',  ( 3.999996093285163035, 28.12756664670878592, 1.519951541579177778 ) ) ;
#3403=CARTESIAN_POINT ( 'NONE',  ( 0.000000000000000000, 28.00000000000000000, -4.000000000000614619 ) ) ;
#3424=VERTEX_POINT ( 'NONE', #9416 ) ;
#3449=ORIENTED_EDGE ( 'NONE', *, *, #10282, .T. ) ;
#3460=EDGE_CURVE ( 'NONE', #4661, #14273, #11305, .T. ) ;
#3471=ADVANCED_FACE ( 'NONE', ( #10884 ), #8404, .T. ) ;
#3507=DIRECTION ( 'NONE',  ( 0.7071067811865465735, 0.7071067811865465735, 5.135208691342337292E-08 ) ) ;
#3540=CARTESIAN_POINT ( 'NONE',  ( 0.000000000000000000, 30.00000000000000000, 0.000000000000000000 ) ) ;
#3545=CARTESIAN_POINT ( 'NONE',  ( 0.000000000000000000, 28.15000000000000213, 0.000000000000000000 ) ) ;
#3562=CARTESIAN_POINT ( 'NONE',  ( 0.000000000000000000, 29.85000000000000142, 0.000000000000000000 ) ) ;
#3571=CARTESIAN_POINT ( 'NONE',  ( -3.999709959627196110, 28.03198827073818578, -0.7544996412928929308 ) ) ;
#3582=ORIENTED_EDGE ( 'NONE', *, *, #12006, .F. ) ;
#3646=CARTESIAN_POINT ( 'NONE',  ( 4.000000000000000888, 29.94682129341588350, 0.9440428258623109192 ) ) ;
#3661=CARTESIAN_POINT ( 'NONE',  ( 0.000000000000000000, 29.85000000000000142, 0.000000000000000000 ) ) ;
#3683=CARTESIAN_POINT ( 'NONE',  ( -3.999996093277206732, 28.12756664670158457, -1.519951541552794883 ) ) ;
#3689=EDGE_LOOP ( 'NONE', ( #14860, #16787, #12860, #8889, #5454, #12201 ) ) ;
#3706=DIRECTION ( 'NONE',  ( -0.5000000000000169864, 0.000000000000000000, -0.8660254037844288266 ) ) ;
#3758=DIRECTION ( 'NONE',  ( 1.000000000000000000, 0.000000000000000000, 0.000000000000000000 ) ) ;
#3782=ORIENTED_EDGE ( 'NONE', *, *, #16185, .T. ) ;
#3812=CARTESIAN_POINT ( 'NONE',  ( -4.000000000000000000, 28.00000000000000000, -2.309401076759000304 ) ) ;
#3847=CIRCLE ( 'NONE', #16228, 2.100000000000000089 ) ;
#3849=EDGE_LOOP ( 'NONE', ( #9322, #10380, #8162 ) ) ;
#3932=DIRECTION ( 'NONE',  ( -1.000000000000000000, 0.000000000000000000, 0.000000000000000000 ) ) ;
#3967=CARTESIAN_POINT ( 'NONE',  ( -4.000000000000057732, 28.25094615492120909, 2.107036910272269470 ) ) ;
#3979=ORIENTED_EDGE ( 'NONE', *, *, #8769, .T. ) ;
#4017=CARTESIAN_POINT ( 'NONE',  ( -1.595510613210902484, 29.99040384242091406, -3.697633671484739537 ) ) ;
#4115=FACE_OUTER_BOUND ( 'NONE', #22570, .T. ) ;
#4120=SURFACE_STYLE_USAGE ( .BOTH. , #17193 ) ;
#4163=VERTEX_POINT ( 'NONE', #16078 ) ;
#4175=CARTESIAN_POINT ( 'NONE',  ( 0.000000000000000000, 28.30000000000000071, 0.000000000000000000 ) ) ;
#4198=CARTESIAN_POINT ( 'NONE',  ( -3.304996520289661177, 29.87418302490023692, 2.710661522857509276 ) ) ;
#4215=VECTOR ( 'NONE', #7239, 1000.000000000000000 ) ;
#4227=B_SPLINE_CURVE_WITH_KNOTS ( 'NONE', 3,
 ( #3184, #10451, #10567, #17951, #12264, #23513, #12501, #8872, #23019, #13074 ),
 .UNSPECIFIED., .F., .F.,
 ( 4, 1, 1, 2, 2, 4 ),
 ( 0.000000000000000000, 0.2500000000000011657, 0.3750000000000013323, 0.4375000000000017208, 0.5000000000000019984, 1.000000000000000000 ),
 .UNSPECIFIED. ) ;
#4233=CARTESIAN_POINT ( 'NONE',  ( -2.000000000000000000, 30.00000000000000000, 3.464101615137999968 ) ) ;
#4248=LINE ( 'NONE', #22994, #14501 ) ;
#4274=EDGE_LOOP ( 'NONE', ( #18213, #19572, #83 ) ) ;
#4327=FACE_OUTER_BOUND ( 'NONE', #15145, .T. ) ;
#4371=CIRCLE ( 'NONE', #11332, 2.100000000000000089 ) ;
#4378=CARTESIAN_POINT ( 'NONE',  ( -1.306994031390691813, 29.96241504948190126, -3.864208797664316020 ) ) ;
#4389=CARTESIAN_POINT ( 'NONE',  ( 2.653270836322024984, 28.03198827073824617, -3.086600612158303392 ) ) ;
#4390=AXIS2_PLACEMENT_3D ( 'NONE', #8983, #23856, #3758 ) ;
#4393=B_SPLINE_CURVE_WITH_KNOTS ( 'NONE', 3,
 ( #134, #20968, #4017, #4378, #13100, #19023, #17207, #18909, #22649, #7523 ),
 .UNSPECIFIED., .F., .F.,
 ( 4, 1, 1, 2, 2, 4 ),
 ( 0.000000000000000000, 0.2499999999999994449, 0.3749999999999994449, 0.4375000000000000000, 0.5000000000000005551, 1.000000000000000000 ),
 .UNSPECIFIED. ) ;
#4408=ORIENTED_EDGE ( 'NONE', *, *, #11941, .T. ) ;
#4520=EDGE_CURVE ( 'NONE', #3424, #6263, #19167, .T. ) ;
#4522=CIRCLE ( 'NONE', #21151, 4.000000000000000000 ) ;
#4549=DIRECTION ( 'NONE',  ( 0.000000000000000000, 1.000000000000000000, 0.000000000000000000 ) ) ;
#4611=LINE ( 'NONE', #2418, #7693 ) ;
#4640=CARTESIAN_POINT ( 'NONE',  ( -2.000000000000000000, 28.00000000000000000, -3.464101615137999968 ) ) ;
#4661=VERTEX_POINT ( 'NONE', #17776 ) ;
#4683=CARTESIAN_POINT ( 'NONE',  ( 4.000000000000000000, 28.30000000000000071, -2.309401076759000304 ) ) ;
#4692=CARTESIAN_POINT ( 'NONE',  ( -4.000000000000000000, 29.69999999999999929, -2.309401076759000304 ) ) ;
#4750=AXIS2_PLACEMENT_3D ( 'NONE', #11185, #16621, #384 ) ;
#4756=CARTESIAN_POINT ( 'NONE',  ( 2.160826008357634720, 29.99999999999999645, -3.371248675920325510 ) ) ;
#4837=ORIENTED_EDGE ( 'NONE', *, *, #9370, .T. ) ;
#4903=B_SPLINE_CURVE_WITH_KNOTS ( 'NONE', 3,
 ( #16305, #5186, #7341, #18149, #12802, #1777, #22005, #23697, #18256, #14834 ),
 .UNSPECIFIED., .F., .F.,
 ( 4, 1, 1, 2, 2, 4 ),
 ( 0.000000000000000000, 0.2500000000000011102, 0.3750000000000014433, 0.4375000000000015543, 0.5000000000000016653, 1.000000000000000000 ),
 .UNSPECIFIED. ) ;
#4912=EDGE_CURVE ( 'NONE', #20571, #8904, #15923, .T. ) ;
#4914=CONICAL_SURFACE ( 'NONE', #21915, 4.309401076758999416, 1.119376321708719590 ) ;
#4922=AXIS2_PLACEMENT_3D ( 'NONE', #8284, #23040, #19429 ) ;
#4952=LINE ( 'NONE', #17421, #21216 ) ;
#5019=AXIS2_PLACEMENT_3D ( 'NONE', #12126, #19513, #10304 ) ;
#5034=LINE ( 'NONE', #6704, #6431 ) ;
#5041=CONICAL_SURFACE ( 'NONE', #10445, 2.249999993254999886, 0.7853981633972997312 ) ;
#5063=ORIENTED_EDGE ( 'NONE', *, *, #19030, .T. ) ;
#5136=DIRECTION ( 'NONE',  ( 1.000000000000000000, 0.000000000000000000, 0.000000000000000000 ) ) ;
#5153=VECTOR ( 'NONE', #23146, 1000.000000000000000 ) ;
#5163=CARTESIAN_POINT ( 'NONE',  ( 2.000000000000000000, 30.00000000000000000, -3.464101615137999968 ) ) ;
#5186=CARTESIAN_POINT ( 'NONE',  ( -0.1784790855350541217, 29.74995697614779644, 4.515757205439222766 ) ) ;
#5207=ORIENTED_EDGE ( 'NONE', *, *, #23608, .T. ) ;
#5241=CARTESIAN_POINT ( 'NONE',  ( 0.000000000000000000, 30.00000000000000000, 4.000000000000621725 ) ) ;
#5269=ADVANCED_FACE ( 'NONE', ( #21454 ), #23373, .T. ) ;
#5281=VERTEX_POINT ( 'NONE', #3295 ) ;
#5299=VERTEX_POINT ( 'NONE', #17705 ) ;
#5318=UNCERTAINTY_MEASURE_WITH_UNIT (LENGTH_MEASURE( 1.000000000000000082E-05 ), #6293, 'distance_accuracy_value', 'NONE');
#5327=B_SPLINE_CURVE_WITH_KNOTS ( 'NONE', 3,
 ( #11513, #15237, #21064, #11747, #10056, #16951, #17439, #20707, #834, #7753 ),
 .UNSPECIFIED., .F., .F.,
 ( 4, 1, 1, 2, 2, 4 ),
 ( 0.000000000000000000, 0.2500000000000013323, 0.3750000000000016098, 0.4375000000000018874, 0.5000000000000021094, 1.000000000000000000 ),
 .UNSPECIFIED. ) ;
#5354=FACE_OUTER_BOUND ( 'NONE', #4274, .T. ) ;
#5361=B_SPLINE_CURVE_WITH_KNOTS ( 'NONE', 3,
 ( #11826, #22595, #20550, #6002, #7714, #13627, #17400, #13386 ),
 .UNSPECIFIED., .F., .F.,
 ( 4, 2, 2, 4 ),
 ( 0.000000000000000000, 0.2500000000000000000, 0.5000000000000000000, 1.000000000000000000 ),
 .UNSPECIFIED. ) ;
#5387=CONICAL_SURFACE ( 'NONE', #2666, 2.249999993279999888, 0.7853981633972997312 ) ;
#5395=AXIS2_PLACEMENT_3D ( 'NONE', #18640, #16577, #1931 ) ;
#5412=DIRECTION ( 'NONE',  ( 1.000000000000000000, 0.000000000000000000, 0.000000000000000000 ) ) ;
#5420=ADVANCED_FACE ( 'NONE', ( #11736, #17429 ), #18992, .T. ) ;
#5426=CIRCLE ( 'NONE', #2712, 4.000000000000000000 ) ;
#5433=CARTESIAN_POINT ( 'NONE',  ( -4.000000000000000000, 28.30000000000000071, 2.309401076759000304 ) ) ;
#5454=ORIENTED_EDGE ( 'NONE', *, *, #8769, .F. ) ;
#5476=EDGE_LOOP ( 'NONE', ( #9949, #18667, #21393 ) ) ;
#5480=LINE ( 'NONE', #20376, #8391 ) ;
#5539=CARTESIAN_POINT ( 'NONE',  ( -2.900806500513820829, 29.93562577624027909, 2.944020739578861789 ) ) ;
#5661=CARTESIAN_POINT ( 'NONE',  ( -4.000000000000000000, 28.30000000000000071, 2.309401076759000304 ) ) ;
#5672=CARTESIAN_POINT ( 'NONE',  ( 2.000000000000000000, 28.00000000000000000, 3.464101615137999968 ) ) ;
#5678=ORIENTED_EDGE ( 'NONE', *, *, #14230, .F. ) ;
#5683=DIRECTION ( 'NONE',  ( 0.000000000000000000, -1.000000000000000000, 0.000000000000000000 ) ) ;
#5692=CARTESIAN_POINT ( 'NONE',  ( 4.000000000000000000, 29.87418302490049626, 1.506880184559475255 ) ) ;
#5694=ORIENTED_EDGE ( 'NONE', *, *, #3460, .T. ) ;
#5714=DIRECTION ( 'NONE',  ( 0.000000000000000000, -1.000000000000000000, 0.000000000000000000 ) ) ;
#5753=CONICAL_SURFACE ( 'NONE', #13476, 2.249999993279999888, 0.7853981633972997312 ) ;
#5754=COLOUR_RGB ( '', 0.09019608, 0.27058824, 0.51372549) ;
#5766=ORIENTED_EDGE ( 'NONE', *, *, #22866, .T. ) ;
#5798=EDGE_CURVE ( 'NONE', #4163, #15215, #23611, .T. ) ;
#5830=DIRECTION ( 'NONE',  ( -1.000000000000000000, 0.000000000000000000, 0.000000000000000000 ) ) ;
#5831=DIRECTION ( 'NONE',  ( 1.000000000000000000, 0.000000000000000000, 0.000000000000000000 ) ) ;
#5859=ORIENTED_EDGE ( 'NONE', *, *, #16643, .F. ) ;
#5860=CARTESIAN_POINT ( 'NONE',  ( -2.100000000000000089, 28.30000000000000071, 0.000000000000000000 ) ) ;
#5869=LINE ( 'NONE', #10653, #1111 ) ;
#5883=CARTESIAN_POINT ( 'NONE',  ( 1.839173991642404582, 30.00000000000000711, 3.556954554355652220 ) ) ;
#5889=CARTESIAN_POINT ( 'NONE',  ( -4.000000000000000000, 29.69999999999999929, 2.309401076759000304 ) ) ;
#5898=CONICAL_SURFACE ( 'NONE', #16736, 4.309401076758999416, 1.119376321708719590 ) ;
#5921=CARTESIAN_POINT ( 'NONE',  ( 4.000000000000000000, 30.00000000000000000, 0.000000000000000000 ) ) ;
#5941=FACE_OUTER_BOUND ( 'NONE', #18670, .T. ) ;
#5979=ORIENTED_EDGE ( 'NONE', *, *, #17236, .T. ) ;
#5980=EDGE_CURVE ( 'NONE', #8904, #14691, #21719, .T. ) ;
#6002=CARTESIAN_POINT ( 'NONE',  ( -0.6838519464012248195, 28.13336607546796841, 4.223839491855484241 ) ) ;
#6015=CARTESIAN_POINT ( 'NONE',  ( 0.000000000000000000, 28.00000000000000000, 0.000000000000000000 ) ) ;
#6059=CARTESIAN_POINT ( 'NONE',  ( -2.329590180155310719, 27.99999999999985079, -3.273812635903178059 ) ) ;
#6075=DIRECTION ( 'NONE',  ( -0.5000000000000169864, 0.000000000000000000, 0.8660254037844289376 ) ) ;
#6104=ADVANCED_FACE ( 'NONE', ( #21570 ), #12369, .T. ) ;
#6133=EDGE_CURVE ( 'NONE', #19752, #9155, #10038, .T. ) ;
#6166=VECTOR ( 'NONE', #1123, 1000.000000000000000 ) ;
#6207=ORIENTED_EDGE ( 'NONE', *, *, #5798, .F. ) ;
#6240=CARTESIAN_POINT ( 'NONE',  ( 1.055729715565287385, 29.92936170367563520, 4.009276318043865750 ) ) ;
#6249=EDGE_LOOP ( 'NONE', ( #598, #23358, #516, #22683 ) ) ;
#6256=FACE_BOUND ( 'NONE', #19308, .T. ) ;
#6263=VERTEX_POINT ( 'NONE', #14864 ) ;
#6273=VERTEX_POINT ( 'NONE', #11129 ) ;
#6281=AXIS2_PLACEMENT_3D ( 'NONE', #1112, #17216, #19150 ) ;
#6293=( LENGTH_UNIT ( ) NAMED_UNIT ( * ) SI_UNIT ( .MILLI., .METRE. ) );
#6340=ORIENTED_EDGE ( 'NONE', *, *, #6133, .F. ) ;
#6414=EDGE_CURVE ( 'NONE', #19423, #16291, #8814, .T. ) ;
#6421=CARTESIAN_POINT ( 'NONE',  ( 0.000000000000000000, 28.15000000674550051, 0.000000000000000000 ) ) ;
#6431=VECTOR ( 'NONE', #8778, 1000.000000000000114 ) ;
#6439=CARTESIAN_POINT ( 'NONE',  ( 4.000000000000000000, 28.30000000000000071, -2.309401076759000304 ) ) ;
#6461=AXIS2_PLACEMENT_3D ( 'NONE', #15981, #23375, #21929 ) ;
#6510=FACE_OUTER_BOUND ( 'NONE', #22420, .T. ) ;
#6519=AXIS2_PLACEMENT_3D ( 'NONE', #10273, #23218, #11933 ) ;
#6652=ORIENTED_EDGE ( 'NONE', *, *, #15572, .F. ) ;
#6670=CIRCLE ( 'NONE', #6281, 2.100000000000000089 ) ;
#6673=( LENGTH_UNIT ( ) NAMED_UNIT ( * ) SI_UNIT ( .MILLI., .METRE. ) );
#6699=ADVANCED_FACE ( 'NONE', ( #6510 ), #5753, .F. ) ;
#6704=CARTESIAN_POINT ( 'NONE',  ( -2.399999988617999680, 29.99999998861800066, -6.349992589004001159E-08 ) ) ;
#6720=ADVANCED_FACE ( 'NONE', ( #16420 ), #2257, .T. ) ;
#6727=CARTESIAN_POINT ( 'NONE',  ( -2.099999992529999915, 28.30000000747030242, -4.159306751197999787E-08 ) ) ;
#6745=EDGE_CURVE ( 'NONE', #6273, #3203, #4903, .T. ) ;
#6747=EDGE_LOOP ( 'NONE', ( #10766, #18000, #11645, #5979 ) ) ;
#6788=ORIENTED_EDGE ( 'NONE', *, *, #22244, .T. ) ;
#6798=B_SPLINE_CURVE_WITH_KNOTS ( 'NONE', 3,
 ( #2369, #5883, #15077, #13382, #22706, #20783, #6240, #17394, #22826, #13622 ),
 .UNSPECIFIED., .F., .F.,
 ( 4, 1, 1, 2, 2, 4 ),
 ( 0.000000000000000000, 0.2499999999999994449, 0.3749999999999994449, 0.4375000000000000000, 0.5000000000000005551, 1.000000000000000000 ),
 .UNSPECIFIED. ) ;
#6827=DIRECTION ( 'NONE',  ( 0.000000000000000000, -1.000000000000000000, 0.000000000000000000 ) ) ;
#6850=ORIENTED_EDGE ( 'NONE', *, *, #4912, .T. ) ;
#6856=DIRECTION ( 'NONE',  ( -0.5000000000000169864, 0.000000000000000000, -0.8660254037844289376 ) ) ;
#6884=VERTEX_POINT ( 'NONE', #3014 ) ;
#6921=( NAMED_UNIT ( * ) PLANE_ANGLE_UNIT ( ) SI_UNIT ( $, .RADIAN. ) );
#6971=EDGE_CURVE ( 'NONE', #8904, #19391, #23137, .T. ) ;
#7013=LINE ( 'NONE', #5661, #4215 ) ;
#7039=AXIS2_PLACEMENT_3D ( 'NONE', #4175, #11687, #15181 ) ;
#7071=CARTESIAN_POINT ( 'NONE',  ( 1.350644574821315613, 28.02555747447238588, -3.839035148326051861 ) ) ;
#7072=ORIENTED_EDGE ( 'NONE', *, *, #15668, .T. ) ;
#7124=CARTESIAN_POINT ( 'NONE',  ( 0.000000000000000000, 15.44510233504000141, 0.000000000000000000 ) ) ;
#7204=ORIENTED_EDGE ( 'NONE', *, *, #18602, .F. ) ;
#7239=DIRECTION ( 'NONE',  ( 0.000000000000000000, 1.000000000000000000, 0.000000000000000000 ) ) ;
#7289=AXIS2_PLACEMENT_3D ( 'NONE', #67, #10755, #22227 ) ;
#7328=AXIS2_PLACEMENT_3D ( 'NONE', #12123, #21322, #3284 ) ;
#7341=CARTESIAN_POINT ( 'NONE',  ( -0.4393762720424909118, 29.81534065533141487, 4.365128144578327429 ) ) ;
#7353=CARTESIAN_POINT ( 'NONE',  ( -4.000000000000000000, 28.00000000000000000, 0.000000000000000000 ) ) ;
#7387=DIRECTION ( 'NONE',  ( 0.000000000000000000, 0.000000000000000000, 1.000000000000000000 ) ) ;
#7393=LINE ( 'NONE', #9457, #11809 ) ;
#7479=CARTESIAN_POINT ( 'NONE',  ( 4.000000000000000000, 29.69999999999999929, 2.309401076759000304 ) ) ;
#7490=EDGE_CURVE ( 'NONE', #8084, #4163, #13899, .T. ) ;
#7519=CARTESIAN_POINT ( 'NONE',  ( -3.316314694148183584, 28.12756664670259354, 2.704122461039521585 ) ) ;
#7523=CARTESIAN_POINT ( 'NONE',  ( 0.000000000000000000, 29.69999999999999929, -4.618802153517000519 ) ) ;
#7597=B_SPLINE_CURVE_WITH_KNOTS ( 'NONE', 3,
 ( #23763, #12752, #20144, #13210, #15133, #7519, #2429, #11525 ),
 .UNSPECIFIED., .F., .F.,
 ( 4, 2, 2, 4 ),
 ( 0.000000000000000000, 0.2500000000000000555, 0.5000000000000001110, 1.000000000000000000 ),
 .UNSPECIFIED. ) ;
#7612=AXIS2_PLACEMENT_3D ( 'NONE', #14996, #22271, #20349 ) ;
#7626=AXIS2_PLACEMENT_3D ( 'NONE', #9706, #7889, #5831 ) ;
#7651=EDGE_LOOP ( 'NONE', ( #19957, #5207, #19886 ) ) ;
#7654=CARTESIAN_POINT ( 'NONE',  ( -3.150855693194152707, 28.10222989789001602, -2.799640769043123978 ) ) ;
#7673=CIRCLE ( 'NONE', #708, 4.000000000000000000 ) ;
#7693=VECTOR ( 'NONE', #19256, 1000.000000000000114 ) ;
#7714=CARTESIAN_POINT ( 'NONE',  ( -0.8491321808595133636, 28.10222989789001957, 4.128541458487867466 ) ) ;
#7753=CARTESIAN_POINT ( 'NONE',  ( -4.000000000000000000, 30.00000000000000000, 0.000000000000000000 ) ) ;
#7766=CARTESIAN_POINT ( 'NONE',  ( 0.9744765624120647063, 29.91693820796410463, -4.056187847889995091 ) ) ;
#7847=CARTESIAN_POINT ( 'NONE',  ( 4.000000000000000000, 29.69999999999999929, 2.309401076759000304 ) ) ;
#7872=ORIENTED_EDGE ( 'NONE', *, *, #23627, .F. ) ;
#7883=CARTESIAN_POINT ( 'NONE',  ( 0.8545932710616226391, 29.89685207198636618, -4.125402498422515052 ) ) ;
#7889=DIRECTION ( 'NONE',  ( 0.000000000000000000, 1.000000000000000000, 0.000000000000000000 ) ) ;
#8021=CARTESIAN_POINT ( 'NONE',  ( 2.327192509895193329, 28.00639765414753057, -3.274853329251975698 ) ) ;
#8084=VERTEX_POINT ( 'NONE', #2571 ) ;
#8133=ORIENTED_EDGE ( 'NONE', *, *, #12006, .T. ) ;
#8145=CARTESIAN_POINT ( 'NONE',  ( 2.000000000000000000, 30.00000000000000000, -3.464101615137999968 ) ) ;
#8162=ORIENTED_EDGE ( 'NONE', *, *, #1138, .F. ) ;
#8203=CARTESIAN_POINT ( 'NONE',  ( 4.000000000000001776, 29.97444252552741872, -0.7494995952805654227 ) ) ;
#8217=VECTOR ( 'NONE', #1854, 1000.000000000000000 ) ;
#8243=ADVANCED_FACE ( 'NONE', ( #5354 ), #14619, .T. ) ;
#8283=CARTESIAN_POINT ( 'NONE',  ( 1.672509921849822945, 28.00639765414753413, 3.652834497693414839 ) ) ;
#8284=CARTESIAN_POINT ( 'NONE',  ( 4.000000000000000000, 28.00000000000000000, 2.309401076759000304 ) ) ;
#8330=ORIENTED_EDGE ( 'NONE', *, *, #333, .T. ) ;
#8359=DIRECTION ( 'NONE',  ( 0.000000000000000000, 1.000000000000000000, 0.000000000000000000 ) ) ;
#8373=B_SPLINE_CURVE_WITH_KNOTS ( 'NONE', 3,
 ( #20398, #16392, #23554, #3571, #23901, #3683, #11073, #14580 ),
 .UNSPECIFIED., .F., .F.,
 ( 4, 2, 2, 4 ),
 ( 0.000000000000000000, 0.2500000000000000555, 0.5000000000000000000, 1.000000000000000000 ),
 .UNSPECIFIED. ) ;
#8391=VECTOR ( 'NONE', #2077, 1000.000000000000000 ) ;
#8392=CARTESIAN_POINT ( 'NONE',  ( 0.000000000000000000, 28.30000000000000071, -4.618802153517000519 ) ) ;
#8404=CONICAL_SURFACE ( 'NONE', #13016, 4.309401076758999416, 1.119376321708719590 ) ;
#8408=CARTESIAN_POINT ( 'NONE',  ( 2.000000000000000000, 28.00000000000000000, 3.464101615137999968 ) ) ;
#8410=PLANE ( 'NONE',  #4922 ) ;
#8428=CARTESIAN_POINT ( 'NONE',  ( 0.000000000000000000, 28.15000000000000213, 0.000000000000000000 ) ) ;
#8430=ORIENTED_EDGE ( 'NONE', *, *, #6414, .T. ) ;
#8457=CARTESIAN_POINT ( 'NONE',  ( 0.000000000000000000, 29.84999999328000087, 0.000000000000000000 ) ) ;
#8528=ADVANCED_FACE ( 'NONE', ( #3165 ), #14296, .T. ) ;
#8529=ORIENTED_EDGE ( 'NONE', *, *, #10279, .F. ) ;
#8558=DIRECTION ( 'NONE',  ( -1.000000000000000000, 0.000000000000000000, 0.000000000000000000 ) ) ;
#8560=CARTESIAN_POINT ( 'NONE',  ( 0.000000000000000000, 29.84999999328000087, -2.249999993279999888 ) ) ;
#8626=ORIENTED_EDGE ( 'NONE', *, *, #12517, .T. ) ;
#8670=CONICAL_SURFACE ( 'NONE', #921, 4.309401076758999416, 1.119376321708719590 ) ;
#8762=B_SPLINE_CURVE_WITH_KNOTS ( 'NONE', 3,
 ( #4683, #19817, #17634, #2861, #14237, #21750, #12186, #3231 ),
 .UNSPECIFIED., .F., .F.,
 ( 4, 2, 2, 4 ),
 ( 0.000000000000000000, 0.2500000000000002220, 0.5000000000000004441, 1.000000000000000000 ),
 .UNSPECIFIED. ) ;
#8769=EDGE_CURVE ( 'NONE', #14273, #23649, #8373, .T. ) ;
#8778=DIRECTION ( 'NONE',  ( 0.7071067811865465735, -0.7071067811865465735, 5.144932599760337753E-08 ) ) ;
#8814=B_SPLINE_CURVE_WITH_KNOTS ( 'NONE', 3,
 ( #7847, #22378, #15214, #16924, #22849, #2639, #444, #20807, #13405, #14981 ),
 .UNSPECIFIED., .F., .F.,
 ( 4, 1, 1, 2, 2, 4 ),
 ( 0.000000000000000000, 0.2500000000000011657, 0.3750000000000013323, 0.4375000000000017208, 0.5000000000000019984, 1.000000000000000000 ),
 .UNSPECIFIED. ) ;
#8872=CARTESIAN_POINT ( 'NONE',  ( -2.649085689637681540, 29.97444252552741872, -3.089351817498231068 ) ) ;
#8873=STYLED_ITEM ( 'NONE', ( #13560 ), #17244 ) ;
#8889=ORIENTED_EDGE ( 'NONE', *, *, #20932, .F. ) ;
#8904=VERTEX_POINT ( 'NONE', #1613 ) ;
#8931=ADVANCED_FACE ( 'NONE', ( #23526 ), #16812, .T. ) ;
#8983=CARTESIAN_POINT ( 'NONE',  ( 0.000000000000000000, 0.000000000000000000, 0.000000000000000000 ) ) ;
#9062=CONICAL_SURFACE ( 'NONE', #1714, 4.309401076758999416, 1.119376321708719590 ) ;
#9101=DIRECTION ( 'NONE',  ( 1.000000000000000000, 0.000000000000000000, 0.000000000000000000 ) ) ;
#9127=CARTESIAN_POINT ( 'NONE',  ( 0.000000000000000000, 28.30000000000000071, -4.618802153517000519 ) ) ;
#9144=CARTESIAN_POINT ( 'NONE',  ( 0.000000000000000000, 29.85000000000000142, 0.000000000000000000 ) ) ;
#9155=VERTEX_POINT ( 'NONE', #9814 ) ;
#9268=AXIS2_PLACEMENT_3D ( 'NONE', #20725, #5714, #20499 ) ;
#9275=VECTOR ( 'NONE', #16329, 1000.000000000000000 ) ;
#9322=ORIENTED_EDGE ( 'NONE', *, *, #13368, .T. ) ;
#9346=CARTESIAN_POINT ( 'NONE',  ( 2.000000000000000000, 30.00000000000000000, -3.464101615137999968 ) ) ;
#9370=EDGE_CURVE ( 'NONE', #15451, #20779, #15419, .T. ) ;
#9416=CARTESIAN_POINT ( 'NONE',  ( 4.000000000000000000, 29.69999999999999929, -2.309401076759000304 ) ) ;
#9422=CARTESIAN_POINT ( 'NONE',  ( 4.000000000000117240, 27.99999999999975486, 0.1904558375517787505 ) ) ;
#9443=DIRECTION ( 'NONE',  ( 0.5000000000000169864, 0.000000000000000000, -0.8660254037844289376 ) ) ;
#9449=LINE ( 'NONE', #20704, #2428 ) ;
#9456=AXIS2_PLACEMENT_3D ( 'NONE', #9725, #17107, #6075 ) ;
#9457=CARTESIAN_POINT ( 'NONE',  ( 0.000000000000000000, 29.85000000000000142, 4.309401076758999416 ) ) ;
#9469=CARTESIAN_POINT ( 'NONE',  ( 0.000000000000000000, 28.00000000000000000, 0.000000000000000000 ) ) ;
#9497=DIRECTION ( 'NONE',  ( 0.000000000000000000, 0.000000000000000000, 1.000000000000000000 ) ) ;
#9529=CARTESIAN_POINT ( 'NONE',  ( -2.693005968609320178, 29.96241504948189416, 3.063994432611676366 ) ) ;
#9547=CIRCLE ( 'NONE', #15720, 4.000000000000000000 ) ;
#9565=DIRECTION ( 'NONE',  ( 0.000000000000000000, -1.000000000000000000, 0.000000000000000000 ) ) ;
#9615=FACE_OUTER_BOUND ( 'NONE', #20049, .T. ) ;
#9636=DIRECTION ( 'NONE',  ( -0.7071067811865465735, -0.7071067811865465735, -5.144932280347337440E-08 ) ) ;
#9647=AXIS2_PLACEMENT_3D ( 'NONE', #15729, #15968, #23117 ) ;
#9687=CARTESIAN_POINT ( 'NONE',  ( 0.000000000000000000, 29.84999999328000087, 0.000000000000000000 ) ) ;
#9692=( NAMED_UNIT ( * ) SI_UNIT ( $, .STERADIAN. ) SOLID_ANGLE_UNIT ( ) );
#9706=CARTESIAN_POINT ( 'NONE',  ( 0.000000000000000000, 15.44510233504000141, 0.000000000000000000 ) ) ;
#9725=CARTESIAN_POINT ( 'NONE',  ( 0.000000000000000000, 28.00000000000000000, 0.000000000000000000 ) ) ;
#9733=APPLICATION_CONTEXT ( 'automotive_design' ) ;
#9761=CONICAL_SURFACE ( 'NONE', #18652, 4.309401076758999416, 1.119376321708719590 ) ;
#9769=ORIENTED_EDGE ( 'NONE', *, *, #22866, .F. ) ;
#9795=( GEOMETRIC_REPRESENTATION_CONTEXT ( 3 ) GLOBAL_UNCERTAINTY_ASSIGNED_CONTEXT ( ( #22026 ) ) GLOBAL_UNIT_ASSIGNED_CONTEXT ( ( #6673, #6921, #23633 ) ) REPRESENTATION_CONTEXT ( 'NONE', 'WORKASPACE' ) );
#9802=EDGE_CURVE ( 'NONE', #3210, #2430, #3106, .T. ) ;
#9814=CARTESIAN_POINT ( 'NONE',  ( -2.399999999999999911, 30.00000000000000000, 0.000000000000000000 ) ) ;
#9816=EDGE_CURVE ( 'NONE', #4661, #22477, #7013, .T. ) ;
#9833=CARTESIAN_POINT ( 'NONE',  ( 2.900806500513820829, 29.93562577624027909, -2.944020739578861789 ) ) ;
#9838=ADVANCED_FACE ( 'NONE', ( #14629 ), #21794, .F. ) ;
#9949=ORIENTED_EDGE ( 'NONE', *, *, #15286, .F. ) ;
#9951=CARTESIAN_POINT ( 'NONE',  ( 3.643546194520566051, 29.79977277844448125, -2.515199777306227347 ) ) ;
#9954=EDGE_LOOP ( 'NONE', ( #5063, #8430, #11255, #15033, #22629, #5678 ) ) ;
#9957=LINE ( 'NONE', #23023, #5153 ) ;
#9965=EDGE_CURVE ( 'NONE', #5281, #5299, #20870, .T. ) ;
#9974=CARTESIAN_POINT ( 'NONE',  ( 2.000000000000000000, 28.00000000000000000, -3.464101615137999968 ) ) ;
#10038=CIRCLE ( 'NONE', #7328, 2.399999999999999911 ) ;
#10056=CARTESIAN_POINT ( 'NONE',  ( -4.000000000000000888, 29.89685207198628092, 1.322601766568780146 ) ) ;
#10132=CARTESIAN_POINT ( 'NONE',  ( -4.000000000000001776, 29.99040384242091761, -0.4670641126940870413 ) ) ;
#10161=EDGE_LOOP ( 'NONE', ( #3782, #6850, #21328, #1530 ) ) ;
#10164=DIRECTION ( 'NONE',  ( 1.000000000000000000, 0.000000000000000000, 0.000000000000000000 ) ) ;
#10198=CARTESIAN_POINT ( 'NONE',  ( 4.000000000000000000, 29.69999999999999929, -2.309401076759000304 ) ) ;
#10202=DIRECTION ( 'NONE',  ( 1.000000000000000000, 0.000000000000000000, 0.000000000000000000 ) ) ;
#10245=CARTESIAN_POINT ( 'NONE',  ( 0.000000000000000000, 30.00000000000000000, 0.000000000000000000 ) ) ;
#10257=DIRECTION ( 'NONE',  ( 0.000000000000000000, -1.000000000000000000, 0.000000000000000000 ) ) ;
#10267=DIRECTION ( 'NONE',  ( -0.5000000000000169864, 0.000000000000000000, 0.8660254037844289376 ) ) ;
#10273=CARTESIAN_POINT ( 'NONE',  ( 0.000000000000000000, 28.30000000000000071, 0.000000000000000000 ) ) ;
#10279=EDGE_CURVE ( 'NONE', #6884, #19752, #12380, .T. ) ;
#10282=EDGE_CURVE ( 'NONE', #12159, #5281, #21254, .T. ) ;
#10284=DIRECTION ( 'NONE',  ( 0.000000000000000000, -1.000000000000000000, 0.000000000000000000 ) ) ;
#10304=DIRECTION ( 'NONE',  ( -1.000000000000000000, 0.000000000000000000, 0.000000000000000000 ) ) ;
#10306=ORIENTED_EDGE ( 'NONE', *, *, #10973, .F. ) ;
#10314=CARTESIAN_POINT ( 'NONE',  ( 0.000000000000000000, 28.00000000000000000, 4.618802153517000519 ) ) ;
#10329=CIRCLE ( 'NONE', #23846, 4.000000000000000000 ) ;
#10380=ORIENTED_EDGE ( 'NONE', *, *, #10564, .T. ) ;
#10413=DIRECTION ( 'NONE',  ( -1.000000000000000000, 0.000000000000000000, 0.000000000000000000 ) ) ;
#10426=DIRECTION ( 'NONE',  ( 0.000000000000000000, 0.000000000000000000, -1.000000000000000000 ) ) ;
#10445=AXIS2_PLACEMENT_3D ( 'NONE', #6421, #15167, #1097 ) ;
#10451=CARTESIAN_POINT ( 'NONE',  ( -3.821520914465098784, 29.74995697614778578, -2.412446024836691461 ) ) ;
#10492=CARTESIAN_POINT ( 'NONE',  ( 0.000000000000000000, 28.00000000000000000, 0.000000000000000000 ) ) ;
#10494=ORIENTED_EDGE ( 'NONE', *, *, #668, .T. ) ;
#10564=EDGE_CURVE ( 'NONE', #19119, #18819, #5361, .T. ) ;
#10567=CARTESIAN_POINT ( 'NONE',  ( -3.560623727957783924, 29.81534065533141131, -2.563075085697513078 ) ) ;
#10580=CONICAL_SURFACE ( 'NONE', #15175, 2.249999993279999888, 0.7853981633972997312 ) ;
#10614=DIRECTION ( 'NONE',  ( -0.5000000000000169864, 0.000000000000000000, 0.8660254037844289376 ) ) ;
#10624=ORIENTED_EDGE ( 'NONE', *, *, #12498, .F. ) ;
#10651=ORIENTED_EDGE ( 'NONE', *, *, #2028, .F. ) ;
#10653=CARTESIAN_POINT ( 'NONE',  ( -2.399999988616999591, 28.00000001138332806, -6.337991255853999810E-08 ) ) ;
#10659=CARTESIAN_POINT ( 'NONE',  ( 0.000000000000000000, 28.30000000000000071, -4.618802153517000519 ) ) ;
#10677=DIRECTION ( 'NONE',  ( 0.5000000000000169864, 0.000000000000000000, 0.8660254037844288266 ) ) ;
#10682=CARTESIAN_POINT ( 'NONE',  ( 0.000000000000000000, 28.15000000000000213, 0.000000000000000000 ) ) ;
#10755=DIRECTION ( 'NONE',  ( 0.000000000000000000, -1.000000000000000000, 0.000000000000000000 ) ) ;
#10766=ORIENTED_EDGE ( 'NONE', *, *, #6971, .T. ) ;
#10775=CARTESIAN_POINT ( 'NONE',  ( 2.000000000000000000, 30.00000000000000000, 3.464101615137999968 ) ) ;
#10789=CARTESIAN_POINT ( 'NONE',  ( 0.000000000000000000, 30.00000000000000000, 0.000000000000000000 ) ) ;
#10793=FACE_OUTER_BOUND ( 'NONE', #12445, .T. ) ;
#10797=CONICAL_SURFACE ( 'NONE', #22003, 2.249999993254999886, 0.7853981633972997312 ) ;
#10832=ADVANCED_BREP_SHAPE_REPRESENTATION ( '', ( #17244, #4390 ), #9795 ) ;
#10836=FACE_OUTER_BOUND ( 'NONE', #5476, .T. ) ;
#10858=CARTESIAN_POINT ( 'NONE',  ( 2.100000000000000089, 29.69999999999999929, 0.000000000000000000 ) ) ;
#10884=FACE_OUTER_BOUND ( 'NONE', #13253, .T. ) ;
#10897=ORIENTED_EDGE ( 'NONE', *, *, #2028, .T. ) ;
#10922=ORIENTED_EDGE ( 'NONE', *, *, #6971, .F. ) ;
#10923=DIRECTION ( 'NONE',  ( 0.000000000000000000, -1.000000000000000000, 0.000000000000000000 ) ) ;
#10973=EDGE_CURVE ( 'NONE', #17884, #20779, #7673, .T. ) ;
#11032=AXIS2_PLACEMENT_3D ( 'NONE', #16088, #14294, #10426 ) ;
#11045=CARTESIAN_POINT ( 'NONE',  ( 0.000000000000000000, 29.85000000000000142, 0.000000000000000000 ) ) ;
#11059=ORIENTED_EDGE ( 'NONE', *, *, #22244, .F. ) ;
#11073=CARTESIAN_POINT ( 'NONE',  ( -4.000000000000073719, 28.20197603011089527, -1.905018119001588683 ) ) ;
#11113=CARTESIAN_POINT ( 'NONE',  ( -2.817565069457256932, 29.94682129341587284, 2.992080202207098694 ) ) ;
#11129=CARTESIAN_POINT ( 'NONE',  ( 0.000000000000000000, 29.69999999999999929, 4.618802153517000519 ) ) ;
#11150=CARTESIAN_POINT ( 'NONE',  ( 0.000000000000000000, 29.85000000000000142, 0.000000000000000000 ) ) ;
#11185=CARTESIAN_POINT ( 'NONE',  ( -4.000000000000000000, 28.00000000000000000, 2.309401076759000304 ) ) ;
#11189=EDGE_CURVE ( 'NONE', #19119, #6273, #4952, .T. ) ;
#11195=AXIS2_PLACEMENT_3D ( 'NONE', #7124, #22245, #18172 ) ;
#11227=DIRECTION ( 'NONE',  ( -0.8660254037844288266, 0.000000000000000000, 0.5000000000000169864 ) ) ;
#11231=ORIENTED_EDGE ( 'NONE', *, *, #23223, .F. ) ;
#11255=ORIENTED_EDGE ( 'NONE', *, *, #15088, .T. ) ;
#11305=B_SPLINE_CURVE_WITH_KNOTS ( 'NONE', 3,
 ( #5433, #3967, #14622, #2026, #14738, #22480, #16786, #7353 ),
 .UNSPECIFIED., .F., .F.,
 ( 4, 2, 2, 4 ),
 ( 0.000000000000000000, 0.2500000000000002220, 0.5000000000000004441, 1.000000000000000000 ),
 .UNSPECIFIED. ) ;
#11332=AXIS2_PLACEMENT_3D ( 'NONE', #11902, #2699, #10202 ) ;
#11344=CARTESIAN_POINT ( 'NONE',  ( 2.399999988617999680, 29.99999998861800066, 6.349992443878999481E-08 ) ) ;
#11392=CARTESIAN_POINT ( 'NONE',  ( 4.000000000000000000, 29.93562577624027199, 1.040161751118763078 ) ) ;
#11512=ORIENTED_EDGE ( 'NONE', *, *, #10564, .F. ) ;
#11513=CARTESIAN_POINT ( 'NONE',  ( -4.000000000000000000, 29.69999999999999929, 2.309401076759000304 ) ) ;
#11523=ORIENTED_EDGE ( 'NONE', *, *, #21982, .T. ) ;
#11525=CARTESIAN_POINT ( 'NONE',  ( -4.000000000000000000, 28.30000000000000071, 2.309401076759000304 ) ) ;
#11559=CARTESIAN_POINT ( 'NONE',  ( 0.000000000000000000, 28.30000000000000071, 0.000000000000000000 ) ) ;
#11645=ORIENTED_EDGE ( 'NONE', *, *, #9965, .F. ) ;
#11647=B_SPLINE_CURVE_WITH_KNOTS ( 'NONE', 3,
 ( #8408, #19552, #8283, #19305, #15647, #21115, #1256, #21361 ),
 .UNSPECIFIED., .F., .F.,
 ( 4, 2, 2, 4 ),
 ( 0.000000000000000000, 0.2499999999999998890, 0.4999999999999997780, 1.000000000000000000 ),
 .UNSPECIFIED. ) ;
#11650=DIRECTION ( 'NONE',  ( 0.000000000000000000, 1.000000000000000000, 0.000000000000000000 ) ) ;
#11687=DIRECTION ( 'NONE',  ( 0.000000000000000000, 1.000000000000000000, 0.000000000000000000 ) ) ;
#11736=FACE_BOUND ( 'NONE', #19907, .T. ) ;
#11744=ADVANCED_FACE ( 'NONE', ( #10793 ), #18544, .T. ) ;
#11747=CARTESIAN_POINT ( 'NONE',  ( -4.000000000000000888, 29.87490599056224383, 1.464369514602714251 ) ) ;
#11751=APPLICATION_CONTEXT ( 'automotive_design' ) ;
#11777=CARTESIAN_POINT ( 'NONE',  ( 2.693005968609320178, 29.96241504948189416, -3.063994432611676366 ) ) ;
#11809=VECTOR ( 'NONE', #13200, 1000.000000000000000 ) ;
#11824=DIRECTION ( 'NONE',  ( -8.117316429522999705E-13, 1.000000000000000000, -5.625591667474000414E-11 ) ) ;
#11826=CARTESIAN_POINT ( 'NONE',  ( 0.000000000000000000, 28.30000000000000071, 4.618802153517000519 ) ) ;
#11892=FACE_OUTER_BOUND ( 'NONE', #18044, .T. ) ;
#11902=CARTESIAN_POINT ( 'NONE',  ( 0.000000000000000000, 29.69999999999999929, 0.000000000000000000 ) ) ;
#11933=DIRECTION ( 'NONE',  ( 1.000000000000000000, 0.000000000000000000, 0.000000000000000000 ) ) ;
#11941=EDGE_CURVE ( 'NONE', #21303, #6884, #22947, .T. ) ;
#11951=DIRECTION ( 'NONE',  ( 0.000000000000000000, 0.7071067811866525998, -0.7071067811864425456 ) ) ;
#11956=CARTESIAN_POINT ( 'NONE',  ( -4.000000000000000000, 30.00000000000000355, -0.1857058784358550652 ) ) ;
#11961=VECTOR ( 'NONE', #11824, 1000.000000000000000 ) ;
#12006=EDGE_CURVE ( 'NONE', #20571, #14280, #23311, .T. ) ;
#12061=CARTESIAN_POINT ( 'NONE',  ( 4.000000000000000000, 28.30000000000000071, 2.309401076759000304 ) ) ;
#12123=CARTESIAN_POINT ( 'NONE',  ( 0.000000000000000000, 30.00000000000000000, 0.000000000000000000 ) ) ;
#12126=CARTESIAN_POINT ( 'NONE',  ( 0.000000000000000000, 30.00000000000000000, 0.000000000000000000 ) ) ;
#12139=ORIENTED_EDGE ( 'NONE', *, *, #17646, .F. ) ;
#12159=VERTEX_POINT ( 'NONE', #19051 ) ;
#12181=ADVANCED_FACE ( 'NONE', ( #13132 ), #20527, .T. ) ;
#12186=CARTESIAN_POINT ( 'NONE',  ( 4.000000000000116351, 27.99999999999975842, -0.3805779584833441365 ) ) ;
#12194=EDGE_CURVE ( 'NONE', #19391, #20571, #3847, .T. ) ;
#12201=ORIENTED_EDGE ( 'NONE', *, *, #3460, .F. ) ;
#12262=CIRCLE ( 'NONE', #1023, 2.399999999999999911 ) ;
#12264=CARTESIAN_POINT ( 'NONE',  ( -3.145406728938545893, 29.89685207198635553, -2.802800731853388960 ) ) ;
#12325=CIRCLE ( 'NONE', #21612, 4.000000000000000000 ) ;
#12369=PLANE ( 'NONE',  #9647 ) ;
#12373=ADVANCED_FACE ( 'NONE', ( #18321 ), #1494, .T. ) ;
#12380=CIRCLE ( 'NONE', #9268, 2.399999999999999911 ) ;
#12410=CARTESIAN_POINT ( 'NONE',  ( -2.000000000000000000, 30.00000000000000000, -3.464101615137999968 ) ) ;
#12445=EDGE_LOOP ( 'NONE', ( #23378, #22588, #23273 ) ) ;
#12498=EDGE_CURVE ( 'NONE', #18819, #4661, #7597, .T. ) ;
#12501=CARTESIAN_POINT ( 'NONE',  ( -3.025523437588010012, 29.91693820796410108, -2.872015382385962656 ) ) ;
#12517=EDGE_CURVE ( 'NONE', #15215, #17884, #23478, .T. ) ;
#12628=DIRECTION ( 'NONE',  ( 0.000000000000000000, 1.000000000000000000, 0.000000000000000000 ) ) ;
#12637=CARTESIAN_POINT ( 'NONE',  ( 0.000000000000000000, 28.15000000674550051, 0.000000000000000000 ) ) ;
#12734=( GEOMETRIC_REPRESENTATION_CONTEXT ( 3 ) GLOBAL_UNCERTAINTY_ASSIGNED_CONTEXT ( ( #5318 ) ) GLOBAL_UNIT_ASSIGNED_CONTEXT ( ( #6293, #17566, #9692 ) ) REPRESENTATION_CONTEXT ( 'NONE', 'WORKASPACE' ) );
#12752=CARTESIAN_POINT ( 'NONE',  ( -2.164939593608601776, 27.99999999999984368, 3.368873696368140713 ) ) ;
#12765=CARTESIAN_POINT ( 'NONE',  ( 0.6838519463944332522, 28.13336607547026702, -4.223839491861407502 ) ) ;
#12781=SHAPE_REPRESENTATION ( 'Stem Lock Nut', ( #4390 ), #9795 ) ;
#12802=CARTESIAN_POINT ( 'NONE',  ( -0.8545932710616226391, 29.89685207198636618, 4.125402498422515052 ) ) ;
#12803=ORIENTED_EDGE ( 'NONE', *, *, #10973, .T. ) ;
#12813=CARTESIAN_POINT ( 'NONE',  ( 4.000000000000000000, 28.30000000000000071, 2.309401076759000304 ) ) ;
#12821=CARTESIAN_POINT ( 'NONE',  ( 4.000000142207500886, 28.05137445130360518, 0.9449696197344532589 ) ) ;
#12860=ORIENTED_EDGE ( 'NONE', *, *, #14438, .T. ) ;
#12883=CARTESIAN_POINT ( 'NONE',  ( -4.000000000000000000, 30.00000000000000000, 0.000000000000000000 ) ) ;
#12920=CARTESIAN_POINT ( 'NONE',  ( -2.100000000000000089, 29.69999999999999929, 0.000000000000000000 ) ) ;
#12927=CARTESIAN_POINT ( 'NONE',  ( 4.000000000000000000, 28.30000000000000071, 2.309401076759000304 ) ) ;
#13016=AXIS2_PLACEMENT_3D ( 'NONE', #22132, #1670, #193 ) ;
#13023=CARTESIAN_POINT ( 'NONE',  ( 0.000000000000000000, 28.00000000000000000, -4.618802153517000519 ) ) ;
#13036=ORIENTED_EDGE ( 'NONE', *, *, #15985, .T. ) ;
#13038=ADVANCED_FACE ( 'NONE', ( #20463 ), #10797, .F. ) ;
#13052=ORIENTED_EDGE ( 'NONE', *, *, #17881, .F. ) ;
#13074=CARTESIAN_POINT ( 'NONE',  ( -2.000000000000000000, 30.00000000000000000, -3.464101615137999968 ) ) ;
#13100=CARTESIAN_POINT ( 'NONE',  ( -1.182434930542719087, 29.94682129341587284, -3.936123028068912344 ) ) ;
#13132=FACE_OUTER_BOUND ( 'NONE', #3689, .T. ) ;
#13161=CARTESIAN_POINT ( 'NONE',  ( 4.000000000000000000, 28.30000000000000071, -2.309401076759000304 ) ) ;
#13172=CARTESIAN_POINT ( 'NONE',  ( 0.000000000000000000, 28.30000000000000071, -2.100000000000000089 ) ) ;
#13183=CARTESIAN_POINT ( 'NONE',  ( 0.000000000000000000, 28.15000000674550051, 0.000000000000000000 ) ) ;
#13200=DIRECTION ( 'NONE',  ( 0.000000000000000000, -0.4362437346113740011, 0.8998285414523820025 ) ) ;
#13210=CARTESIAN_POINT ( 'NONE',  ( -2.653270836322014770, 28.03198827073824972, 3.086600612158311385 ) ) ;
#13250=CIRCLE ( 'NONE', #1288, 4.000000000000000000 ) ;
#13253=EDGE_LOOP ( 'NONE', ( #3979, #21948, #22542 ) ) ;
#13277=ORIENTED_EDGE ( 'NONE', *, *, #954, .F. ) ;
#13286=CIRCLE ( 'NONE', #16759, 4.000000000000000000 ) ;
#13323=CARTESIAN_POINT ( 'NONE',  ( 0.4393762720424909118, 29.81534065533141487, -4.365128144578327429 ) ) ;
#13327=CYLINDRICAL_SURFACE ( 'NONE', #7626, 2.100000000000000089 ) ;
#13368=EDGE_CURVE ( 'NONE', #20052, #19119, #11647, .T. ) ;
#13382=CARTESIAN_POINT ( 'NONE',  ( 1.306994031390691813, 29.96241504948190126, 3.864208797664316020 ) ) ;
#13386=CARTESIAN_POINT ( 'NONE',  ( -2.000000000000000000, 28.00000000000000000, 3.464101615137999968 ) ) ;
#13405=CARTESIAN_POINT ( 'NONE',  ( 2.321186682587942141, 30.00000000000000000, 3.278664397485417048 ) ) ;
#13443=CARTESIAN_POINT ( 'NONE',  ( 0.9358744650684699407, 29.91068681084918879, -4.078474779182606369 ) ) ;
#13476=AXIS2_PLACEMENT_3D ( 'NONE', #8457, #15580, #21410 ) ;
#13488=ORIENTED_EDGE ( 'NONE', *, *, #14968, .F. ) ;
#13560=PRESENTATION_STYLE_ASSIGNMENT (( #4120 ) ) ;
#13581=CARTESIAN_POINT ( 'NONE',  ( 2.944270284434496787, 29.92936170367566717, -2.918926912232259419 ) ) ;
#13622=CARTESIAN_POINT ( 'NONE',  ( 0.000000000000000000, 29.69999999999999929, 4.618802153517000519 ) ) ;
#13627=CARTESIAN_POINT ( 'NONE',  ( -1.350644574833474776, 28.02555747447238943, 3.839035148322985425 ) ) ;
#13633=EDGE_CURVE ( 'NONE', #20779, #15215, #4393, .T. ) ;
#13652=EDGE_CURVE ( 'NONE', #23649, #8084, #13909, .T. ) ;
#13663=ADVANCED_FACE ( 'NONE', ( #5941 ), #13327, .F. ) ;
#13674=CARTESIAN_POINT ( 'NONE',  ( 0.000000000000000000, 28.30000000000000071, 4.618802153517000519 ) ) ;
#13698=EDGE_LOOP ( 'NONE', ( #23158, #8626, #5766, #11231, #19877, #16589 ) ) ;
#13712=ORIENTED_EDGE ( 'NONE', *, *, #23639, .T. ) ;
#13725=CARTESIAN_POINT ( 'NONE',  ( -4.000000000000000000, 29.69999999999999929, 2.309401076759000304 ) ) ;
#13828=CARTESIAN_POINT ( 'NONE',  ( 2.164939593608602220, 27.99999999999984368, -3.368873696368142490 ) ) ;
#13899=B_SPLINE_CURVE_WITH_KNOTS ( 'NONE', 3,
 ( #4640, #23518, #990, #15877, #21227, #23267, #18079, #8392 ),
 .UNSPECIFIED., .F., .F.,
 ( 4, 2, 2, 4 ),
 ( 0.000000000000000000, 0.2500000000000002220, 0.5000000000000004441, 1.000000000000000000 ),
 .UNSPECIFIED. ) ;
#13909=B_SPLINE_CURVE_WITH_KNOTS ( 'NONE', 3,
 ( #2192, #14906, #2553, #22424, #7654, #20500, #6059, #2080 ),
 .UNSPECIFIED., .F., .F.,
 ( 4, 2, 2, 4 ),
 ( 0.000000000000000000, 0.2499999999999998890, 0.4999999999999997780, 1.000000000000000000 ),
 .UNSPECIFIED. ) ;
#13988=FACE_OUTER_BOUND ( 'NONE', #19431, .T. ) ;
#14065=CIRCLE ( 'NONE', #22556, 4.000000000000000000 ) ;
#14070=DIRECTION ( 'NONE',  ( 0.000000000000000000, -1.000000000000000000, 0.000000000000000000 ) ) ;
#14222=B_SPLINE_CURVE_WITH_KNOTS ( 'NONE', 3,
 ( #12813, #20090, #20203, #19740, #19967, #1320, #21899, #14505 ),
 .UNSPECIFIED., .F., .F.,
 ( 4, 2, 2, 4 ),
 ( 0.000000000000000000, 0.2500000000000000000, 0.5000000000000000000, 1.000000000000000000 ),
 .UNSPECIFIED. ) ;
#14230=EDGE_CURVE ( 'NONE', #2430, #20052, #14222, .T. ) ;
#14237=CARTESIAN_POINT ( 'NONE',  ( 3.999987874060709991, 28.10222989788994497, -1.328900689436832261 ) ) ;
#14244=EDGE_LOOP ( 'NONE', ( #23705, #3162, #4837 ) ) ;
#14267=EDGE_CURVE ( 'NONE', #3203, #22477, #18551, .T. ) ;
#14273=VERTEX_POINT ( 'NONE', #22131 ) ;
#14280=VERTEX_POINT ( 'NONE', #12920 ) ;
#14294=DIRECTION ( 'NONE',  ( 0.000000000000000000, 1.000000000000000000, 0.000000000000000000 ) ) ;
#14296=PLANE ( 'NONE',  #2645 ) ;
#14300=AXIS2_PLACEMENT_3D ( 'NONE', #3812, #3932, #9497 ) ;
#14315=FACE_OUTER_BOUND ( 'NONE', #20845, .T. ) ;
#14333=VERTEX_POINT ( 'NONE', #13161 ) ;
#14336=CARTESIAN_POINT ( 'NONE',  ( 0.000000000000000000, 28.00000000000000000, 0.000000000000000000 ) ) ;
#14414=ORIENTED_EDGE ( 'NONE', *, *, #4520, .T. ) ;
#14419=DIRECTION ( 'NONE',  ( 0.000000000000000000, -1.000000000000000000, 0.000000000000000000 ) ) ;
#14438=EDGE_CURVE ( 'NONE', #15451, #19406, #594, .T. ) ;
#14444=DIRECTION ( 'NONE',  ( 0.000000000000000000, 0.000000000000000000, 1.000000000000000000 ) ) ;
#14479=ORIENTED_EDGE ( 'NONE', *, *, #13633, .F. ) ;
#14501=VECTOR ( 'NONE', #8359, 1000.000000000000000 ) ;
#14505=CARTESIAN_POINT ( 'NONE',  ( 2.000000000000000000, 28.00000000000000000, 3.464101615137999968 ) ) ;
#14572=ORIENTED_EDGE ( 'NONE', *, *, #11189, .T. ) ;
#14580=CARTESIAN_POINT ( 'NONE',  ( -4.000000000000000000, 28.30000000000000071, -2.309401076759000304 ) ) ;
#14591=ORIENTED_EDGE ( 'NONE', *, *, #22878, .T. ) ;
#14614=AXIS2_PLACEMENT_3D ( 'NONE', #22983, #10284, #10413 ) ;
#14619=CONICAL_SURFACE ( 'NONE', #15004, 4.309401076758999416, 1.119376321708719590 ) ;
#14622=CARTESIAN_POINT ( 'NONE',  ( -3.999895459877826465, 28.20780860099995024, 1.909390889640791622 ) ) ;
#14629=FACE_OUTER_BOUND ( 'NONE', #18903, .T. ) ;
#14660=CARTESIAN_POINT ( 'NONE',  ( 4.000000000000000000, 29.69999999999999929, 2.309401076759000304 ) ) ;
#14690=CARTESIAN_POINT ( 'NONE',  ( 0.8491321808655799552, 28.10222989789001247, -4.128541458486335358 ) ) ;
#14691=VERTEX_POINT ( 'NONE', #10858 ) ;
#14738=CARTESIAN_POINT ( 'NONE',  ( -3.999987874060712656, 28.10222989788994497, 1.328900689436825377 ) ) ;
#14767=SHAPE_REPRESENTATION_RELATIONSHIP ( 'NONE' , 'NONE' ,  #12781, #10832 ) ;
#14796=DIRECTION ( 'NONE',  ( -1.000000000000000000, 0.000000000000000000, 0.000000000000000000 ) ) ;
#14834=CARTESIAN_POINT ( 'NONE',  ( -2.000000000000000000, 30.00000000000000000, 3.464101615137999968 ) ) ;
#14859=CARTESIAN_POINT ( 'NONE',  ( 0.000000000000000000, 30.00000000000000000, 0.000000000000000000 ) ) ;
#14860=ORIENTED_EDGE ( 'NONE', *, *, #9816, .T. ) ;
#14864=CARTESIAN_POINT ( 'NONE',  ( 4.000000000000000000, 30.00000000000000000, 0.000000000000000000 ) ) ;
#14886=CARTESIAN_POINT ( 'NONE',  ( 4.000000000000000888, 29.92936170367563520, 1.090349405812182537 ) ) ;
#14906=CARTESIAN_POINT ( 'NONE',  ( -3.824747491000654698, 28.25094615491947181, -2.410583160005970171 ) ) ;
#14914=DIRECTION ( 'NONE',  ( 0.000000000000000000, -1.000000000000000000, 0.000000000000000000 ) ) ;
#14968=EDGE_CURVE ( 'NONE', #21303, #14691, #21584, .T. ) ;
#14981=CARTESIAN_POINT ( 'NONE',  ( 2.000000000000000000, 30.00000000000000000, 3.464101615137999968 ) ) ;
#14990=DIRECTION ( 'NONE',  ( 0.000000000000000000, 0.000000000000000000, -1.000000000000000000 ) ) ;
#14996=CARTESIAN_POINT ( 'NONE',  ( 0.000000000000000000, 28.00000000000000000, 0.000000000000000000 ) ) ;
#15004=AXIS2_PLACEMENT_3D ( 'NONE', #3545, #12628, #18209 ) ;
#15033=ORIENTED_EDGE ( 'NONE', *, *, #11189, .F. ) ;
#15036=CARTESIAN_POINT ( 'NONE',  ( 0.000000000000000000, 28.15000000674550051, -2.249999993254999886 ) ) ;
#15063=ORIENTED_EDGE ( 'NONE', *, *, #10279, .T. ) ;
#15077=CARTESIAN_POINT ( 'NONE',  ( 1.595510613210902484, 29.99040384242091051, 3.697633671484739537 ) ) ;
#15088=EDGE_CURVE ( 'NONE', #16291, #6273, #6798, .T. ) ;
#15133=CARTESIAN_POINT ( 'NONE',  ( -2.818367767609784469, 28.05137445130671381, 2.991616928423204147 ) ) ;
#15145=EDGE_LOOP ( 'NONE', ( #11523, #6788, #421, #17150, #15917, #8330, #16457 ) ) ;
#15149=DIRECTION ( 'NONE',  ( 0.000000000000000000, -1.000000000000000000, 0.000000000000000000 ) ) ;
#15167=DIRECTION ( 'NONE',  ( 0.000000000000000000, -1.000000000000000000, 0.000000000000000000 ) ) ;
#15175=AXIS2_PLACEMENT_3D ( 'NONE', #22653, #19275, #23014 ) ;
#15181=DIRECTION ( 'NONE',  ( -1.000000000000000000, 0.000000000000000000, 0.000000000000000000 ) ) ;
#15198=CIRCLE ( 'NONE', #18322, 2.399999999999999911 ) ;
#15202=CARTESIAN_POINT ( 'NONE',  ( -2.000000000000000000, 30.00000000000000000, 3.464101615137999968 ) ) ;
#15206=CARTESIAN_POINT ( 'NONE',  ( 4.000000000000000888, 30.00000000000001066, -0.3708744353061897425 ) ) ;
#15214=CARTESIAN_POINT ( 'NONE',  ( 3.560623727957783924, 29.81534065533141131, 2.563075085697513078 ) ) ;
#15215=VERTEX_POINT ( 'NONE', #3232 ) ;
#15227=CARTESIAN_POINT ( 'NONE',  ( 0.000000000000000000, 30.00000000000000000, 0.000000000000000000 ) ) ;
#15237=CARTESIAN_POINT ( 'NONE',  ( -4.000000000000000000, 29.74995697614769341, 2.103311180602513542 ) ) ;
#15251=CARTESIAN_POINT ( 'NONE',  ( 0.000000000000000000, 29.69999999999999929, -4.618802153517000519 ) ) ;
#15286=EDGE_CURVE ( 'NONE', #18824, #16291, #4522, .T. ) ;
#15295=EDGE_CURVE ( 'NONE', #14273, #8084, #9547, .T. ) ;
#15408=ORIENTED_EDGE ( 'NONE', *, *, #13633, .T. ) ;
#15419=CIRCLE ( 'NONE', #5019, 4.000000000000000000 ) ;
#15451=VERTEX_POINT ( 'NONE', #12883 ) ;
#15457=DIRECTION ( 'NONE',  ( -0.000000000000000000, 1.000000000000000000, 0.000000000000000000 ) ) ;
#15475=EDGE_LOOP ( 'NONE', ( #20752, #12139, #10897, #2023, #21786, #20131, #12803 ) ) ;
#15543=AXIS2_PLACEMENT_3D ( 'NONE', #31, #15149, #20388 ) ;
#15572=EDGE_CURVE ( 'NONE', #19752, #14691, #658, .T. ) ;
#15580=DIRECTION ( 'NONE',  ( 0.000000000000000000, 1.000000000000000000, 0.000000000000000000 ) ) ;
#15647=CARTESIAN_POINT ( 'NONE',  ( 1.181632374602280988, 28.05137445130629104, 3.936586548167761990 ) ) ;
#15668=EDGE_CURVE ( 'NONE', #5299, #12159, #12262, .T. ) ;
#15681=CARTESIAN_POINT ( 'NONE',  ( -4.000000000000000000, 30.00000000000000000, 0.000000000000000000 ) ) ;
#15686=CARTESIAN_POINT ( 'NONE',  ( 4.000000000000000000, 29.74995697614769341, -2.103311180602513542 ) ) ;
#15695=ADVANCED_FACE ( 'NONE', ( #13988 ), #4914, .T. ) ;
#15720=AXIS2_PLACEMENT_3D ( 'NONE', #17761, #1164, #8558 ) ;
#15729=CARTESIAN_POINT ( 'NONE',  ( 4.000000000000000000, 28.00000000000000000, -2.309401076759000304 ) ) ;
#15863=ORIENTED_EDGE ( 'NONE', *, *, #18962, .F. ) ;
#15877=CARTESIAN_POINT ( 'NONE',  ( -1.346439123299412177, 28.03198827073827459, -3.841100253456362523 ) ) ;
#15882=CARTESIAN_POINT ( 'NONE',  ( 2.099999992529999915, 28.30000000747030242, 4.159306788217000353E-08 ) ) ;
#15917=ORIENTED_EDGE ( 'NONE', *, *, #15295, .T. ) ;
#15923=CIRCLE ( 'NONE', #7039, 2.100000000000000089 ) ;
#15968=DIRECTION ( 'NONE',  ( 0.5000000000000169864, 0.000000000000000000, -0.8660254037844288266 ) ) ;
#15981=CARTESIAN_POINT ( 'NONE',  ( 0.000000000000000000, 28.15000000000000213, 0.000000000000000000 ) ) ;
#15985=EDGE_CURVE ( 'NONE', #19406, #20779, #4227, .T. ) ;
#16034=B_SPLINE_CURVE_WITH_KNOTS ( 'NONE', 3,
 ( #5921, #23860, #16946, #18653, #3646, #11392, #14886, #5692, #2059, #14660 ),
 .UNSPECIFIED., .F., .F.,
 ( 4, 1, 1, 2, 2, 4 ),
 ( 0.000000000000000000, 0.2500000000000002776, 0.3750000000000006106, 0.4375000000000007216, 0.5000000000000009992, 1.000000000000000000 ),
 .UNSPECIFIED. ) ;
#16078=CARTESIAN_POINT ( 'NONE',  ( 0.000000000000000000, 28.30000000000000071, -4.618802153517000519 ) ) ;
#16088=CARTESIAN_POINT ( 'NONE',  ( 0.000000000000000000, 28.15000000000000213, 0.000000000000000000 ) ) ;
#16172=CARTESIAN_POINT ( 'NONE',  ( 0.000000000000000000, 28.00000000000000000, 0.000000000000000000 ) ) ;
#16185=EDGE_CURVE ( 'NONE', #12159, #20571, #5869, .T. ) ;
#16197=ORIENTED_EDGE ( 'NONE', *, *, #23223, .T. ) ;
#16216=CIRCLE ( 'NONE', #20106, 4.000000000000000000 ) ;
#16228=AXIS2_PLACEMENT_3D ( 'NONE', #11559, #16871, #17119 ) ;
#16251=CARTESIAN_POINT ( 'NONE',  ( -2.000000000000000000, 28.00000000000000000, 3.464101615137999968 ) ) ;
#16261=ORIENTED_EDGE ( 'NONE', *, *, #14230, .T. ) ;
#16291=VERTEX_POINT ( 'NONE', #10775 ) ;
#16305=CARTESIAN_POINT ( 'NONE',  ( 0.000000000000000000, 29.69999999999999929, 4.618802153517000519 ) ) ;
#16326=CARTESIAN_POINT ( 'NONE',  ( 4.000000000000000000, 28.00000000000000000, 0.000000000000000000 ) ) ;
#16329=DIRECTION ( 'NONE',  ( 0.000000000000000000, 1.000000000000000000, 0.000000000000000000 ) ) ;
#16383=CARTESIAN_POINT ( 'NONE',  ( 2.000000000000000000, 28.00000000000000000, -3.464101615137999968 ) ) ;
#16392=CARTESIAN_POINT ( 'NONE',  ( -4.000000000000115463, 27.99999999999976552, -0.1904558375376560198 ) ) ;
#16420=FACE_OUTER_BOUND ( 'NONE', #17443, .T. ) ;
#16457=ORIENTED_EDGE ( 'NONE', *, *, #22692, .T. ) ;
#16501=CARTESIAN_POINT ( 'NONE',  ( 0.3463667137627760018, 28.20780860099773335, -4.418706525551467479 ) ) ;
#16562=CARTESIAN_POINT ( 'NONE',  ( 4.000000000000071942, 28.20197603011810372, 1.905018119031321566 ) ) ;
#16573=DIRECTION ( 'NONE',  ( 0.000000000000000000, 1.000000000000000000, 0.000000000000000000 ) ) ;
#16577=DIRECTION ( 'NONE',  ( 0.000000000000000000, -1.000000000000000000, 0.000000000000000000 ) ) ;
#16589=ORIENTED_EDGE ( 'NONE', *, *, #946, .F. ) ;
#16621=DIRECTION ( 'NONE',  ( -0.5000000000000169864, 0.000000000000000000, 0.8660254037844288266 ) ) ;
#16624=EDGE_CURVE ( 'NONE', #6263, #16291, #12325, .T. ) ;
#16643=EDGE_CURVE ( 'NONE', #22477, #15451, #5327, .T. ) ;
#16651=ADVANCED_FACE ( 'NONE', ( #4115 ), #5387, .F. ) ;
#16655=AXIS2_PLACEMENT_3D ( 'NONE', #10314, #10677, #14419 ) ;
#16733=ORIENTED_EDGE ( 'NONE', *, *, #6745, .T. ) ;
#16736=AXIS2_PLACEMENT_3D ( 'NONE', #11150, #9565, #7387 ) ;
#16754=PRODUCT_DEFINITION_CONTEXT ( 'detailed design', #9733, 'design' ) ;
#16759=AXIS2_PLACEMENT_3D ( 'NONE', #16172, #10257, #6856 ) ;
#16786=CARTESIAN_POINT ( 'NONE',  ( -4.000000000000116351, 27.99999999999975842, 0.3805779584833383633 ) ) ;
#16787=ORIENTED_EDGE ( 'NONE', *, *, #16643, .T. ) ;
#16793=CARTESIAN_POINT ( 'NONE',  ( 3.999709959623201971, 28.03198827073818933, 0.7544996413140969693 ) ) ;
#16812=CONICAL_SURFACE ( 'NONE', #1364, 4.309401076758999416, 1.119376321708719590 ) ;
#16859=CONICAL_SURFACE ( 'NONE', #22643, 2.249999993254999886, 0.7853981633972997312 ) ;
#16871=DIRECTION ( 'NONE',  ( 0.000000000000000000, 1.000000000000000000, 0.000000000000000000 ) ) ;
#16874=ADVANCED_FACE ( 'NONE', ( #6256, #4327 ), #19093, .F. ) ;
#16924=CARTESIAN_POINT ( 'NONE',  ( 3.268181200173220002, 29.87490599056235041, 2.731916857836431234 ) ) ;
#16934=EDGE_LOOP ( 'NONE', ( #17863, #13036, #15408, #6207, #1382, #216 ) ) ;
#16946=CARTESIAN_POINT ( 'NONE',  ( 4.000000000000000000, 29.99040384242091051, 0.4670641126941218468 ) ) ;
#16951=CARTESIAN_POINT ( 'NONE',  ( -3.999999999999999112, 29.91068681084913905, 1.228746328088897721 ) ) ;
#16984=ORIENTED_EDGE ( 'NONE', *, *, #9965, .T. ) ;
#17068=DIRECTION ( 'NONE',  ( 0.000000000000000000, 0.000000000000000000, -1.000000000000000000 ) ) ;
#17107=DIRECTION ( 'NONE',  ( 0.000000000000000000, -1.000000000000000000, 0.000000000000000000 ) ) ;
#17119=DIRECTION ( 'NONE',  ( 1.000000000000000000, 0.000000000000000000, 0.000000000000000000 ) ) ;
#17128=PRODUCT ( 'Stem Lock Nut', 'Stem Lock Nut', '', ( #20293 ) ) ;
#17150=ORIENTED_EDGE ( 'NONE', *, *, #18602, .T. ) ;
#17157=CARTESIAN_POINT ( 'NONE',  ( 4.000000000000000000, 29.69999999999999929, -2.309401076759000304 ) ) ;
#17193=SURFACE_SIDE_STYLE ('',( #22520 ) ) ;
#17207=CARTESIAN_POINT ( 'NONE',  ( -1.055729715565287385, 29.92936170367563520, -4.009276318043865750 ) ) ;
#17216=DIRECTION ( 'NONE',  ( 0.000000000000000000, -1.000000000000000000, 0.000000000000000000 ) ) ;
#17236=EDGE_CURVE ( 'NONE', #5281, #8904, #4611, .T. ) ;
#17244=MANIFOLD_SOLID_BREP ( 'Stock-MAS-673-1', #21243 ) ;
#17247=B_SPLINE_CURVE_WITH_KNOTS ( 'NONE', 3,
 ( #9127, #142, #16501, #12765, #14690, #7071, #1511, #16383 ),
 .UNSPECIFIED., .F., .F.,
 ( 4, 2, 2, 4 ),
 ( 0.000000000000000000, 0.2499999999999998890, 0.4999999999999997780, 1.000000000000000000 ),
 .UNSPECIFIED. ) ;
#17296=EDGE_LOOP ( 'NONE', ( #16197, #14414, #771, #23658, #21722, #13052 ) ) ;
#17394=CARTESIAN_POINT ( 'NONE',  ( 0.6950034797113092688, 29.87418302490042876, 4.217541707417931107 ) ) ;
#17400=CARTESIAN_POINT ( 'NONE',  ( -1.670409819853669209, 27.99999999999984013, 3.654390594367815215 ) ) ;
#17409=CARTESIAN_POINT ( 'NONE',  ( 4.000000000000000888, 29.87490599056224383, -1.464369514602714251 ) ) ;
#17421=CARTESIAN_POINT ( 'NONE',  ( 0.000000000000000000, 28.30000000000000071, 4.618802153517000519 ) ) ;
#17429=FACE_OUTER_BOUND ( 'NONE', #15475, .T. ) ;
#17439=CARTESIAN_POINT ( 'NONE',  ( -4.000000000000000000, 29.91693820796410108, 1.184172465503444904 ) ) ;
#17443=EDGE_LOOP ( 'NONE', ( #19172, #9769, #13712 ) ) ;
#17566=( NAMED_UNIT ( * ) PLANE_ANGLE_UNIT ( ) SI_UNIT ( $, .RADIAN. ) );
#17629=CARTESIAN_POINT ( 'NONE',  ( 0.000000000000000000, 28.15000000000000213, 0.000000000000000000 ) ) ;
#17634=CARTESIAN_POINT ( 'NONE',  ( 3.999895459877826465, 28.20780860099995024, -1.909390889640790512 ) ) ;
#17646=EDGE_CURVE ( 'NONE', #3203, #15451, #16216, .T. ) ;
#17705=CARTESIAN_POINT ( 'NONE',  ( 0.000000000000000000, 28.00000000000000000, -2.400000000000455991 ) ) ;
#17719=CARTESIAN_POINT ( 'NONE',  ( 2.818367767609802677, 28.05137445130671381, -2.991616928423186828 ) ) ;
#17761=CARTESIAN_POINT ( 'NONE',  ( 0.000000000000000000, 28.00000000000000000, 0.000000000000000000 ) ) ;
#17776=CARTESIAN_POINT ( 'NONE',  ( -4.000000000000000000, 28.30000000000000071, 2.309401076759000304 ) ) ;
#17863=ORIENTED_EDGE ( 'NONE', *, *, #20932, .T. ) ;
#17881=EDGE_CURVE ( 'NONE', #14333, #3210, #8762, .T. ) ;
#17884=VERTEX_POINT ( 'NONE', #5163 ) ;
#17951=CARTESIAN_POINT ( 'NONE',  ( -3.268181200173220002, 29.87490599056235041, -2.731916857836431234 ) ) ;
#17970=DIRECTION ( 'NONE',  ( 0.000000000000000000, -1.000000000000000000, 0.000000000000000000 ) ) ;
#18000=ORIENTED_EDGE ( 'NONE', *, *, #22681, .T. ) ;
#18016=ADVANCED_FACE ( 'NONE', ( #23124 ), #5041, .F. ) ;
#18044=EDGE_LOOP ( 'NONE', ( #1372, #23848, #6652, #8529 ) ) ;
#18068=DIRECTION ( 'NONE',  ( 0.000000000000000000, 1.000000000000000000, 0.000000000000000000 ) ) ;
#18079=CARTESIAN_POINT ( 'NONE',  ( -0.3502059142650872370, 28.20197603011382981, -4.416610674644638301 ) ) ;
#18142=CARTESIAN_POINT ( 'NONE',  ( 0.000000000000000000, 28.00000000000000000, 0.000000000000000000 ) ) ;
#18149=CARTESIAN_POINT ( 'NONE',  ( -0.7318187998270078154, 29.87490599056237528, 4.196286372439439027 ) ) ;
#18172=DIRECTION ( 'NONE',  ( 1.000000000000000000, 0.000000000000000000, 0.000000000000000000 ) ) ;
#18191=AXIS2_PLACEMENT_3D ( 'NONE', #9469, #11650, #5830 ) ;
#18209=DIRECTION ( 'NONE',  ( 0.000000000000000000, 0.000000000000000000, -1.000000000000000000 ) ) ;
#18213=ORIENTED_EDGE ( 'NONE', *, *, #23467, .T. ) ;
#18256=CARTESIAN_POINT ( 'NONE',  ( -1.678813317411953054, 30.00000000000000355, 3.649538832790644616 ) ) ;
#18321=FACE_OUTER_BOUND ( 'NONE', #19602, .T. ) ;
#18322=AXIS2_PLACEMENT_3D ( 'NONE', #3333, #14914, #14796 ) ;
#18332=DIRECTION ( 'NONE',  ( 0.000000000000000000, 0.000000000000000000, 1.000000000000000000 ) ) ;
#18447=PLANE ( 'NONE',  #4750 ) ;
#18544=CONICAL_SURFACE ( 'NONE', #5395, 4.309401076758999416, 1.119376321708719590 ) ;
#18551=B_SPLINE_CURVE_WITH_KNOTS ( 'NONE', 3,
 ( #15202, #18730, #2139, #9529, #11113, #5539, #22479, #4198, #22362, #5889 ),
 .UNSPECIFIED., .F., .F.,
 ( 4, 1, 1, 2, 2, 4 ),
 ( 0.000000000000000000, 0.2499999999999996669, 0.3749999999999997224, 0.4374999999999996114, 0.4999999999999995559, 1.000000000000000000 ),
 .UNSPECIFIED. ) ;
#18588=DIRECTION ( 'NONE',  ( 0.000000000000000000, 0.000000000000000000, 1.000000000000000000 ) ) ;
#18594=EDGE_LOOP ( 'NONE', ( #5859, #21003, #19653 ) ) ;
#18602=EDGE_CURVE ( 'NONE', #18819, #14273, #1732, .T. ) ;
#18640=CARTESIAN_POINT ( 'NONE',  ( 0.000000000000000000, 29.85000000000000142, 0.000000000000000000 ) ) ;
#18642=DIRECTION ( 'NONE',  ( 0.000000000000000000, -1.000000000000000000, 0.000000000000000000 ) ) ;
#18652=AXIS2_PLACEMENT_3D ( 'NONE', #3562, #6827, #18332 ) ;
#18653=CARTESIAN_POINT ( 'NONE',  ( 4.000000000000000888, 29.96241504948190482, 0.8002143650531877705 ) ) ;
#18667=ORIENTED_EDGE ( 'NONE', *, *, #18962, .T. ) ;
#18670=EDGE_LOOP ( 'NONE', ( #8133, #7872, #3352, #23022 ) ) ;
#18682=LINE ( 'NONE', #15036, #8217 ) ;
#18730=CARTESIAN_POINT ( 'NONE',  ( -2.160826008357634720, 29.99999999999999645, 3.371248675920325510 ) ) ;
#18779=CONICAL_SURFACE ( 'NONE', #20348, 4.309401076758999416, 1.119376321708719590 ) ;
#18819=VERTEX_POINT ( 'NONE', #16251 ) ;
#18824=VERTEX_POINT ( 'NONE', #5241 ) ;
#18903=EDGE_LOOP ( 'NONE', ( #23516, #13488, #21125, #3582, #3252, #10922 ) ) ;
#18904=CARTESIAN_POINT ( 'NONE',  ( 1.350914310362234527, 29.97444252552742583, -3.838851412777819938 ) ) ;
#18909=CARTESIAN_POINT ( 'NONE',  ( -0.6950034797113092688, 29.87418302490042876, -4.217541707417931107 ) ) ;
#18962=EDGE_CURVE ( 'NONE', #18824, #6273, #7393, .T. ) ;
#18972=ORIENTED_EDGE ( 'NONE', *, *, #6745, .F. ) ;
#18992=PLANE ( 'NONE',  #22835 ) ;
#18995=CARTESIAN_POINT ( 'NONE',  ( 4.000000000000000000, 28.00000000000000000, 0.000000000000000000 ) ) ;
#19023=CARTESIAN_POINT ( 'NONE',  ( -1.099193499486128323, 29.93562577624026488, -3.984182490697167900 ) ) ;
#19030=EDGE_CURVE ( 'NONE', #2430, #19423, #4248, .T. ) ;
#19051=CARTESIAN_POINT ( 'NONE',  ( -2.399999999999999911, 28.00000000000000000, 0.000000000000000000 ) ) ;
#19086=CARTESIAN_POINT ( 'NONE',  ( 4.000000000000000888, 29.89685207198628092, -1.322601766568780146 ) ) ;
#19093=PLANE ( 'NONE',  #715 ) ;
#19119=VERTEX_POINT ( 'NONE', #13674 ) ;
#19142=CONICAL_SURFACE ( 'NONE', #11032, 4.309401076758999416, 1.119376321708719590 ) ;
#19150=DIRECTION ( 'NONE',  ( -1.000000000000000000, 0.000000000000000000, 0.000000000000000000 ) ) ;
#19167=B_SPLINE_CURVE_WITH_KNOTS ( 'NONE', 3,
 ( #17157, #15686, #552, #17409, #19086, #1046, #802, #8203, #15206, #22957 ),
 .UNSPECIFIED., .F., .F.,
 ( 4, 1, 1, 2, 2, 4 ),
 ( 0.000000000000000000, 0.2500000000000013323, 0.3750000000000016098, 0.4375000000000018874, 0.5000000000000021094, 1.000000000000000000 ),
 .UNSPECIFIED. ) ;
#19172=ORIENTED_EDGE ( 'NONE', *, *, #4520, .F. ) ;
#19196=ADVANCED_FACE ( 'NONE', ( #1212 ), #19142, .T. ) ;
#19208=CARTESIAN_POINT ( 'NONE',  ( -3.999999999999999112, 29.94682129341587995, -0.9440428258622635127 ) ) ;
#19216=CONICAL_SURFACE ( 'NONE', #6461, 4.309401076758999416, 1.119376321708719590 ) ;
#19256=DIRECTION ( 'NONE',  ( -0.7071067811865465735, 0.7071067811865465735, -5.135208680714336970E-08 ) ) ;
#19275=DIRECTION ( 'NONE',  ( 0.000000000000000000, 1.000000000000000000, 0.000000000000000000 ) ) ;
#19305=CARTESIAN_POINT ( 'NONE',  ( 1.346439123301719665, 28.03198827073827459, 3.841100253455552060 ) ) ;
#19308=EDGE_LOOP ( 'NONE', ( #16984, #7072, #3449 ) ) ;
#19328=DIRECTION ( 'NONE',  ( 0.000000000000000000, 0.000000000000000000, -1.000000000000000000 ) ) ;
#19340=VERTEX_POINT ( 'NONE', #3403 ) ;
#19391=VERTEX_POINT ( 'NONE', #13172 ) ;
#19406=VERTEX_POINT ( 'NONE', #22374 ) ;
#19423=VERTEX_POINT ( 'NONE', #7479 ) ;
#19429=DIRECTION ( 'NONE',  ( 0.000000000000000000, 1.000000000000000000, 0.000000000000000000 ) ) ;
#19431=EDGE_LOOP ( 'NONE', ( #327, #5694, #7204 ) ) ;
#19513=DIRECTION ( 'NONE',  ( 0.000000000000000000, -1.000000000000000000, 0.000000000000000000 ) ) ;
#19534=CARTESIAN_POINT ( 'NONE',  ( 3.316314694148171593, 28.12756664670257933, -2.704122461039529579 ) ) ;
#19550=DIRECTION ( 'NONE',  ( 0.000000000000000000, 0.000000000000000000, -1.000000000000000000 ) ) ;
#19552=CARTESIAN_POINT ( 'NONE',  ( 1.835060406389813270, 27.99999999999983658, 3.559329533908949461 ) ) ;
#19572=ORIENTED_EDGE ( 'NONE', *, *, #17881, .T. ) ;
#19602=EDGE_LOOP ( 'NONE', ( #10306, #3172, #14479 ) ) ;
#19615=CIRCLE ( 'NONE', #7612, 4.000000000000000000 ) ;
#19638=ORIENTED_EDGE ( 'NONE', *, *, #6133, .T. ) ;
#19653=ORIENTED_EDGE ( 'NONE', *, *, #17646, .T. ) ;
#19680=AXIS2_PLACEMENT_3D ( 'NONE', #3661, #23529, #14444 ) ;
#19737=CARTESIAN_POINT ( 'NONE',  ( 0.000000000000000000, 29.69999999999999929, -2.100000000000000089 ) ) ;
#19740=CARTESIAN_POINT ( 'NONE',  ( 3.316026328257057010, 28.13336607546882817, 2.704152903937933061 ) ) ;
#19752=VERTEX_POINT ( 'NONE', #593 ) ;
#19817=CARTESIAN_POINT ( 'NONE',  ( 4.000000000000060396, 28.25094615492120198, -2.107036910272262809 ) ) ;
#19877=ORIENTED_EDGE ( 'NONE', *, *, #23467, .F. ) ;
#19886=ORIENTED_EDGE ( 'NONE', *, *, #946, .T. ) ;
#19907=EDGE_LOOP ( 'NONE', ( #2084, #15063, #19638 ) ) ;
#19957=ORIENTED_EDGE ( 'NONE', *, *, #22692, .F. ) ;
#19967=CARTESIAN_POINT ( 'NONE',  ( 3.150855693196132457, 28.10222989789001602, 2.799640769041085164 ) ) ;
#19977=CARTESIAN_POINT ( 'NONE',  ( 3.999702431745993270, 28.00639765414744886, 0.3779811684581091957 ) ) ;
#20049=EDGE_LOOP ( 'NONE', ( #15863, #10651, #18972 ) ) ;
#20052=VERTEX_POINT ( 'NONE', #5672 ) ;
#20085=MECHANICAL_DESIGN_GEOMETRIC_PRESENTATION_REPRESENTATION('',(#8873),#12734);
#20090=CARTESIAN_POINT ( 'NONE',  ( 3.824747490998164245, 28.25094615491878614, 2.410583160007404580 ) ) ;
#20106=AXIS2_PLACEMENT_3D ( 'NONE', #23586, #2764, #10267 ) ;
#20131=ORIENTED_EDGE ( 'NONE', *, *, #23639, .F. ) ;
#20144=CARTESIAN_POINT ( 'NONE',  ( -2.327192509895188000, 28.00639765414752702, 3.274853329251978362 ) ) ;
#20200=ORIENTED_EDGE ( 'NONE', *, *, #7490, .T. ) ;
#20203=CARTESIAN_POINT ( 'NONE',  ( 3.653528746108709147, 28.20780860099632648, 2.509315635922550580 ) ) ;
#20224=DIRECTION ( 'NONE',  ( 0.5000000000000169864, 0.000000000000000000, -0.8660254037844289376 ) ) ;
#20293=PRODUCT_CONTEXT ( 'NONE', #11751, 'mechanical' ) ;
#20348=AXIS2_PLACEMENT_3D ( 'NONE', #9144, #22564, #18588 ) ;
#20349=DIRECTION ( 'NONE',  ( 0.5000000000000169864, 0.000000000000000000, -0.8660254037844289376 ) ) ;
#20374=CARTESIAN_POINT ( 'NONE',  ( 1.678813317411953054, 30.00000000000000355, -3.649538832790644616 ) ) ;
#20376=CARTESIAN_POINT ( 'NONE',  ( -4.000000000000000000, 28.30000000000000071, -2.309401076759000304 ) ) ;
#20385=B_SPLINE_CURVE_WITH_KNOTS ( 'NONE', 3,
 ( #8145, #4756, #2442, #11777, #2561, #9833, #13581, #2818, #9951, #10198 ),
 .UNSPECIFIED., .F., .F.,
 ( 4, 1, 1, 2, 2, 4 ),
 ( 0.000000000000000000, 0.2499999999999996669, 0.3749999999999997224, 0.4374999999999996114, 0.4999999999999995559, 1.000000000000000000 ),
 .UNSPECIFIED. ) ;
#20388=DIRECTION ( 'NONE',  ( -0.5000000000000169864, 0.000000000000000000, -0.8660254037844289376 ) ) ;
#20398=CARTESIAN_POINT ( 'NONE',  ( -4.000000000000000000, 28.00000000000000000, 0.000000000000000000 ) ) ;
#20463=FACE_OUTER_BOUND ( 'NONE', #6249, .T. ) ;
#20495=CARTESIAN_POINT ( 'NONE',  ( 0.1784790855350541217, 29.74995697614779644, -4.515757205439222766 ) ) ;
#20499=DIRECTION ( 'NONE',  ( -1.000000000000000000, 0.000000000000000000, 0.000000000000000000 ) ) ;
#20500=CARTESIAN_POINT ( 'NONE',  ( -2.649379677059598759, 28.02555747447239654, -3.089210087443399200 ) ) ;
#20507=FACE_OUTER_BOUND ( 'NONE', #20911, .T. ) ;
#20511=ADVANCED_FACE ( 'NONE', ( #9615 ), #18779, .T. ) ;
#20527=PLANE ( 'NONE',  #14300 ) ;
#20550=CARTESIAN_POINT ( 'NONE',  ( -0.3463667137703017040, 28.20780860099542053, 4.418706525546099328 ) ) ;
#20571=VERTEX_POINT ( 'NONE', #5860 ) ;
#20578=CARTESIAN_POINT ( 'NONE',  ( -4.000000000000000000, 28.30000000000000071, -2.309401076759000304 ) ) ;
#20704=CARTESIAN_POINT ( 'NONE',  ( 4.000000000000000000, 28.30000000000000071, -2.309401076759000304 ) ) ;
#20707=CARTESIAN_POINT ( 'NONE',  ( -4.000000000000001776, 29.97444252552741872, 0.7494995952805654227 ) ) ;
#20712=ADVANCED_FACE ( 'NONE', ( #23765 ), #16859, .F. ) ;
#20725=CARTESIAN_POINT ( 'NONE',  ( 0.000000000000000000, 30.00000000000000000, 0.000000000000000000 ) ) ;
#20752=ORIENTED_EDGE ( 'NONE', *, *, #9370, .F. ) ;
#20779=VERTEX_POINT ( 'NONE', #12410 ) ;
#20783=CARTESIAN_POINT ( 'NONE',  ( 1.099193499486128323, 29.93562577624026488, 3.984182490697167900 ) ) ;
#20807=CARTESIAN_POINT ( 'NONE',  ( 2.649085689637681540, 29.97444252552741872, 3.089351817498231068 ) ) ;
#20845=EDGE_LOOP ( 'NONE', ( #21062, #22956, #20200 ) ) ;
#20870=CIRCLE ( 'NONE', #23587, 2.399999999999999911 ) ;
#20911=EDGE_LOOP ( 'NONE', ( #14572, #16733, #255, #1790, #10624, #11512 ) ) ;
#20932=EDGE_CURVE ( 'NONE', #23649, #19406, #5480, .T. ) ;
#20968=CARTESIAN_POINT ( 'NONE',  ( -1.839173991642404582, 30.00000000000000711, -3.556954554355652220 ) ) ;
#21003=ORIENTED_EDGE ( 'NONE', *, *, #14267, .F. ) ;
#21062=ORIENTED_EDGE ( 'NONE', *, *, #23608, .F. ) ;
#21064=CARTESIAN_POINT ( 'NONE',  ( -4.000000000000000000, 29.81534065533123723, 1.802053058880664471 ) ) ;
#21094=CARTESIAN_POINT ( 'NONE',  ( 0.000000000000000000, 28.00000000000000000, 0.000000000000000000 ) ) ;
#21115=CARTESIAN_POINT ( 'NONE',  ( 0.6836813991273753555, 28.12756664670376594, 4.224074002598932509 ) ) ;
#21125=ORIENTED_EDGE ( 'NONE', *, *, #22878, .F. ) ;
#21135=DIRECTION ( 'NONE',  ( 0.000000000000000000, 1.000000000000000000, 0.000000000000000000 ) ) ;
#21151=AXIS2_PLACEMENT_3D ( 'NONE', #10245, #21510, #10614 ) ;
#21207=ORIENTED_EDGE ( 'NONE', *, *, #668, .F. ) ;
#21216=VECTOR ( 'NONE', #815, 1000.000000000000000 ) ;
#21227=CARTESIAN_POINT ( 'NONE',  ( -1.181632374603358793, 28.05137445130588603, -3.936586548166617572 ) ) ;
#21243=CLOSED_SHELL ( 'NONE', ( #2498, #22582, #6699, #18016, #13663, #20712, #13038, #9838, #23755, #16651, #20511, #5420, #12373, #8931, #23282, #6720, #11744, #21665, #6104, #8528, #12181, #22780, #21852, #5269, #2918, #3471, #15695, #8243, #19196, #16874 ) ) ;
#21254=CIRCLE ( 'NONE', #18191, 2.399999999999999911 ) ;
#21282=CARTESIAN_POINT ( 'NONE',  ( -3.999999999999999112, 29.79977277844470862, -1.897803675662255163 ) ) ;
#21303=VERTEX_POINT ( 'NONE', #19737 ) ;
#21322=DIRECTION ( 'NONE',  ( 0.000000000000000000, -1.000000000000000000, 0.000000000000000000 ) ) ;
#21328=ORIENTED_EDGE ( 'NONE', *, *, #17236, .F. ) ;
#21361=CARTESIAN_POINT ( 'NONE',  ( 0.000000000000000000, 28.30000000000000071, 4.618802153517000519 ) ) ;
#21393=ORIENTED_EDGE ( 'NONE', *, *, #15088, .F. ) ;
#21410=DIRECTION ( 'NONE',  ( 0.000000000000000000, 0.000000000000000000, -1.000000000000000000 ) ) ;
#21454=FACE_OUTER_BOUND ( 'NONE', #9954, .T. ) ;
#21483=DIRECTION ( 'NONE',  ( 0.000000000000000000, -1.000000000000000000, 0.000000000000000000 ) ) ;
#21510=DIRECTION ( 'NONE',  ( 0.000000000000000000, 1.000000000000000000, 0.000000000000000000 ) ) ;
#21570=FACE_OUTER_BOUND ( 'NONE', #13698, .T. ) ;
#21584=CIRCLE ( 'NONE', #14614, 2.100000000000000089 ) ;
#21612=AXIS2_PLACEMENT_3D ( 'NONE', #3540, #10923, #9101 ) ;
#21630=VERTEX_POINT ( 'NONE', #9974 ) ;
#21665=ADVANCED_FACE ( 'NONE', ( #2717 ), #8410, .T. ) ;
#21719=LINE ( 'NONE', #15882, #6166 ) ;
#21722=ORIENTED_EDGE ( 'NONE', *, *, #9802, .F. ) ;
#21750=CARTESIAN_POINT ( 'NONE',  ( 4.000024251878890880, 28.02555747447231127, -0.7498250608958110242 ) ) ;
#21761=SHAPE_DEFINITION_REPRESENTATION ( #689, #12781 ) ;
#21786=ORIENTED_EDGE ( 'NONE', *, *, #16624, .F. ) ;
#21794=CYLINDRICAL_SURFACE ( 'NONE', #11195, 2.100000000000000089 ) ;
#21852=ADVANCED_FACE ( 'NONE', ( #3297 ), #19216, .T. ) ;
#21899=CARTESIAN_POINT ( 'NONE',  ( 2.329590180150573175, 27.99999999999984013, 3.273812635905912316 ) ) ;
#21915=AXIS2_PLACEMENT_3D ( 'NONE', #8428, #1159, #19328 ) ;
#21929=DIRECTION ( 'NONE',  ( 0.000000000000000000, 0.000000000000000000, -1.000000000000000000 ) ) ;
#21948=ORIENTED_EDGE ( 'NONE', *, *, #13652, .T. ) ;
#21982=EDGE_CURVE ( 'NONE', #21630, #3210, #19615, .T. ) ;
#22003=AXIS2_PLACEMENT_3D ( 'NONE', #13183, #18642, #14990 ) ;
#22005=CARTESIAN_POINT ( 'NONE',  ( -0.9744765624120647063, 29.91693820796410463, 4.056187847889995091 ) ) ;
#22026=UNCERTAINTY_MEASURE_WITH_UNIT (LENGTH_MEASURE( 1.000000000000000082E-05 ), #6673, 'distance_accuracy_value', 'NONE');
#22067=DIRECTION ( 'NONE',  ( 0.000000000000000000, -1.000000000000000000, 0.000000000000000000 ) ) ;
#22131=CARTESIAN_POINT ( 'NONE',  ( -4.000000000000000000, 28.00000000000000000, 0.000000000000000000 ) ) ;
#22132=CARTESIAN_POINT ( 'NONE',  ( 0.000000000000000000, 28.15000000000000213, 0.000000000000000000 ) ) ;
#22227=DIRECTION ( 'NONE',  ( 0.000000000000000000, 0.000000000000000000, 1.000000000000000000 ) ) ;
#22244=EDGE_CURVE ( 'NONE', #3210, #20052, #10329, .T. ) ;
#22245=DIRECTION ( 'NONE',  ( 0.000000000000000000, 1.000000000000000000, 0.000000000000000000 ) ) ;
#22271=DIRECTION ( 'NONE',  ( 0.000000000000000000, -1.000000000000000000, 0.000000000000000000 ) ) ;
#22277=ORIENTED_EDGE ( 'NONE', *, *, #9802, .T. ) ;
#22304=ORIENTED_EDGE ( 'NONE', *, *, #15572, .T. ) ;
#22362=CARTESIAN_POINT ( 'NONE',  ( -3.643546194520566051, 29.79977277844448125, 2.515199777306227347 ) ) ;
#22374=CARTESIAN_POINT ( 'NONE',  ( -4.000000000000000000, 29.69999999999999929, -2.309401076759000304 ) ) ;
#22378=CARTESIAN_POINT ( 'NONE',  ( 3.821520914465098784, 29.74995697614778578, 2.412446024836691461 ) ) ;
#22420=EDGE_LOOP ( 'NONE', ( #14591, #4408, #13277, #10494 ) ) ;
#22424=CARTESIAN_POINT ( 'NONE',  ( -3.316026328260925471, 28.13336607546986556, -2.704152903936609231 ) ) ;
#22477=VERTEX_POINT ( 'NONE', #13725 ) ;
#22479=CARTESIAN_POINT ( 'NONE',  ( -2.944270284434496787, 29.92936170367566717, 2.918926912232259419 ) ) ;
#22480=CARTESIAN_POINT ( 'NONE',  ( -4.000024251878890880, 28.02555747447231127, 0.7498250608958049179 ) ) ;
#22513=DIRECTION ( 'NONE',  ( 0.000000000000000000, 1.000000000000000000, 0.000000000000000000 ) ) ;
#22520=SURFACE_STYLE_FILL_AREA ( #2795 ) ;
#22542=ORIENTED_EDGE ( 'NONE', *, *, #15295, .F. ) ;
#22556=AXIS2_PLACEMENT_3D ( 'NONE', #21094, #14070, #3186 ) ;
#22564=DIRECTION ( 'NONE',  ( 0.000000000000000000, -1.000000000000000000, 0.000000000000000000 ) ) ;
#22570=EDGE_LOOP ( 'NONE', ( #22304, #848, #21207, #6340 ) ) ;
#22582=ADVANCED_FACE ( 'NONE', ( #10836 ), #9761, .T. ) ;
#22588=ORIENTED_EDGE ( 'NONE', *, *, #23253, .F. ) ;
#22595=CARTESIAN_POINT ( 'NONE',  ( -0.1752525090037950484, 28.25094615491813599, 4.517620070267612142 ) ) ;
#22629=ORIENTED_EDGE ( 'NONE', *, *, #13368, .F. ) ;
#22643=AXIS2_PLACEMENT_3D ( 'NONE', #12637, #21483, #19550 ) ;
#22649=CARTESIAN_POINT ( 'NONE',  ( -0.3564538054804340383, 29.79977277844466954, -4.413003452969196161 ) ) ;
#22653=CARTESIAN_POINT ( 'NONE',  ( 0.000000000000000000, 29.84999999328000087, 0.000000000000000000 ) ) ;
#22673=VECTOR ( 'NONE', #9636, 1000.000000000000114 ) ;
#22681=EDGE_CURVE ( 'NONE', #19391, #5299, #18682, .T. ) ;
#22683=ORIENTED_EDGE ( 'NONE', *, *, #15668, .F. ) ;
#22692=EDGE_CURVE ( 'NONE', #19340, #21630, #2408, .T. ) ;
#22706=CARTESIAN_POINT ( 'NONE',  ( 1.182434930542719087, 29.94682129341587284, 3.936123028068912344 ) ) ;
#22740=CARTESIAN_POINT ( 'NONE',  ( 0.000000000000000000, 30.00000000000000000, 0.000000000000000000 ) ) ;
#22780=ADVANCED_FACE ( 'NONE', ( #20507 ), #18447, .T. ) ;
#22826=CARTESIAN_POINT ( 'NONE',  ( 0.3564538054804340383, 29.79977277844466954, 4.413003452969196161 ) ) ;
#22833=CARTESIAN_POINT ( 'NONE',  ( -4.000000000000000000, 29.93562577624027554, -1.040161751118715117 ) ) ;
#22835=AXIS2_PLACEMENT_3D ( 'NONE', #22740, #456, #10164 ) ;
#22849=CARTESIAN_POINT ( 'NONE',  ( 3.145406728938545893, 29.89685207198635553, 2.802800731853388960 ) ) ;
#22866=EDGE_CURVE ( 'NONE', #17884, #3424, #20385, .T. ) ;
#22878=EDGE_CURVE ( 'NONE', #14280, #21303, #6670, .T. ) ;
#22947=LINE ( 'NONE', #8560, #1141 ) ;
#22956=ORIENTED_EDGE ( 'NONE', *, *, #333, .F. ) ;
#22957=CARTESIAN_POINT ( 'NONE',  ( 4.000000000000000000, 30.00000000000000000, 0.000000000000000000 ) ) ;
#22983=CARTESIAN_POINT ( 'NONE',  ( 0.000000000000000000, 29.69999999999999929, 0.000000000000000000 ) ) ;
#22994=CARTESIAN_POINT ( 'NONE',  ( 4.000000000000000000, 28.30000000000000071, 2.309401076759000304 ) ) ;
#22995=FILL_AREA_STYLE_COLOUR ( '', #5754 ) ;
#23014=DIRECTION ( 'NONE',  ( 0.000000000000000000, 0.000000000000000000, -1.000000000000000000 ) ) ;
#23019=CARTESIAN_POINT ( 'NONE',  ( -2.321186682587942141, 30.00000000000000355, -3.278664397485417048 ) ) ;
#23022=ORIENTED_EDGE ( 'NONE', *, *, #4912, .F. ) ;
#23023=CARTESIAN_POINT ( 'NONE',  ( 0.000000000000000000, 28.15000000000000213, -4.309401076758999416 ) ) ;
#23040=DIRECTION ( 'NONE',  ( 1.000000000000000000, 0.000000000000000000, 0.000000000000000000 ) ) ;
#23117=DIRECTION ( 'NONE',  ( 0.000000000000000000, -1.000000000000000000, 0.000000000000000000 ) ) ;
#23124=FACE_OUTER_BOUND ( 'NONE', #6747, .T. ) ;
#23137=CIRCLE ( 'NONE', #6519, 2.100000000000000089 ) ;
#23146=DIRECTION ( 'NONE',  ( 0.000000000000000000, 0.4362437346113740011, -0.8998285414523820025 ) ) ;
#23158=ORIENTED_EDGE ( 'NONE', *, *, #5798, .T. ) ;
#23186=DIRECTION ( 'NONE',  ( 0.000000000000000000, 0.000000000000000000, -1.000000000000000000 ) ) ;
#23200=CARTESIAN_POINT ( 'NONE',  ( -4.000000000000000888, 29.96241504948189771, -0.8002143650531428065 ) ) ;
#23218=DIRECTION ( 'NONE',  ( 0.000000000000000000, 1.000000000000000000, 0.000000000000000000 ) ) ;
#23223=EDGE_CURVE ( 'NONE', #14333, #3424, #9449, .T. ) ;
#23253=EDGE_CURVE ( 'NONE', #6263, #19423, #16034, .T. ) ;
#23267=CARTESIAN_POINT ( 'NONE',  ( -0.6836813991252411737, 28.12756664670459728, -4.224074002601208910 ) ) ;
#23273=ORIENTED_EDGE ( 'NONE', *, *, #16624, .T. ) ;
#23282=ADVANCED_FACE ( 'NONE', ( #2295 ), #5898, .T. ) ;
#23311=LINE ( 'NONE', #6727, #11961 ) ;
#23358=ORIENTED_EDGE ( 'NONE', *, *, #12194, .T. ) ;
#23373=PLANE ( 'NONE',  #16655 ) ;
#23375=DIRECTION ( 'NONE',  ( 0.000000000000000000, 1.000000000000000000, 0.000000000000000000 ) ) ;
#23378=ORIENTED_EDGE ( 'NONE', *, *, #6414, .F. ) ;
#23467=EDGE_CURVE ( 'NONE', #21630, #14333, #23845, .T. ) ;
#23478=B_SPLINE_CURVE_WITH_KNOTS ( 'NONE', 3,
 ( #15251, #20495, #13323, #1961, #7883, #13443, #7766, #18904, #20374, #9346 ),
 .UNSPECIFIED., .F., .F.,
 ( 4, 1, 1, 2, 2, 4 ),
 ( 0.000000000000000000, 0.2500000000000011102, 0.3750000000000014433, 0.4375000000000015543, 0.5000000000000016653, 1.000000000000000000 ),
 .UNSPECIFIED. ) ;
#23513=CARTESIAN_POINT ( 'NONE',  ( -3.064125534931650296, 29.91068681084918168, -2.849728451093327397 ) ) ;
#23516=ORIENTED_EDGE ( 'NONE', *, *, #5980, .T. ) ;
#23518=CARTESIAN_POINT ( 'NONE',  ( -1.835060406388425713, 27.99999999999984723, -3.559329533909752818 ) ) ;
#23526=FACE_OUTER_BOUND ( 'NONE', #14244, .T. ) ;
#23529=DIRECTION ( 'NONE',  ( 0.000000000000000000, -1.000000000000000000, 0.000000000000000000 ) ) ;
#23554=CARTESIAN_POINT ( 'NONE',  ( -3.999702431747993003, 28.00639765414744531, -0.3779811684369214220 ) ) ;
#23586=CARTESIAN_POINT ( 'NONE',  ( 0.000000000000000000, 30.00000000000000000, 0.000000000000000000 ) ) ;
#23587=AXIS2_PLACEMENT_3D ( 'NONE', #18142, #23804, #5412 ) ;
#23608=EDGE_CURVE ( 'NONE', #19340, #4163, #9957, .T. ) ;
#23611=LINE ( 'NONE', #10659, #9275 ) ;
#23627=EDGE_CURVE ( 'NONE', #14691, #14280, #4371, .T. ) ;
#23633=( NAMED_UNIT ( * ) SI_UNIT ( $, .STERADIAN. ) SOLID_ANGLE_UNIT ( ) );
#23639=EDGE_CURVE ( 'NONE', #17884, #6263, #13250, .T. ) ;
#23649=VERTEX_POINT ( 'NONE', #20578 ) ;
#23658=ORIENTED_EDGE ( 'NONE', *, *, #19030, .F. ) ;
#23697=CARTESIAN_POINT ( 'NONE',  ( -1.350914310362234527, 29.97444252552742583, 3.838851412777819938 ) ) ;
#23705=ORIENTED_EDGE ( 'NONE', *, *, #15985, .F. ) ;
#23755=ADVANCED_FACE ( 'NONE', ( #11892 ), #10580, .F. ) ;
#23763=CARTESIAN_POINT ( 'NONE',  ( -2.000000000000000000, 28.00000000000000000, 3.464101615137999968 ) ) ;
#23765=FACE_OUTER_BOUND ( 'NONE', #10161, .T. ) ;
#23804=DIRECTION ( 'NONE',  ( 0.000000000000000000, 1.000000000000000000, 0.000000000000000000 ) ) ;
#23845=B_SPLINE_CURVE_WITH_KNOTS ( 'NONE', 3,
 ( #260, #13828, #8021, #4389, #17719, #19534, #989, #6439 ),
 .UNSPECIFIED., .F., .F.,
 ( 4, 2, 2, 4 ),
 ( 0.000000000000000000, 0.2500000000000002776, 0.5000000000000005551, 1.000000000000000000 ),
 .UNSPECIFIED. ) ;
#23846=AXIS2_PLACEMENT_3D ( 'NONE', #14336, #17970, #5136 ) ;
#23848=ORIENTED_EDGE ( 'NONE', *, *, #14968, .T. ) ;
#23856=DIRECTION ( 'NONE',  ( 0.000000000000000000, 0.000000000000000000, 1.000000000000000000 ) ) ;
#23860=CARTESIAN_POINT ( 'NONE',  ( 4.000000000000000000, 29.99999999999999645, 0.1857058784358717463 ) ) ;
#23901=CARTESIAN_POINT ( 'NONE',  ( -4.000000142211483478, 28.05137445130720408, -0.9449696197475782045 ) ) ;
ENDSEC;
END-ISO-10303-21;
